ISO-10303-21;
HEADER;
/* Generated by software containing ST-Developer
 * from STEP Tools, Inc. (www.steptools.com) 
 */

FILE_DESCRIPTION(
/* description */ ('Independent hinged machine back cover with retained hinge pins, perim
eter gasket and quarter-turn cam latch. Nominal cover 360 x 260 x 3 mm
, frame 430 x 300 x 20 mm. No guarding, structural or ingress rating a
ssigned.'),
/* implementation_level */ '2;1');

FILE_NAME(
/* name */ 'Socket head cap screw M4x8.step',
/* time_stamp */ '2026-11-09T19:36:59-08:00',
/* author */ (''),
/* organization */ (''),
/* preprocessor_version */ 'ST-DEVELOPER v20.2',
/* originating_system */ 'Autodesk Translation Framework v15.17.0.0',
/* authorisation */ '');

FILE_SCHEMA (('AUTOMOTIVE_DESIGN { 1 0 10303 214 3 1 1 }'));
ENDSEC;

DATA;
#10=MECHANICAL_DESIGN_GEOMETRIC_PRESENTATION_REPRESENTATION('',(#206),#32627);
#159=CONICAL_SURFACE('',#9248,1.5,0.785398163397448);
#170=SHAPE_REPRESENTATION_RELATIONSHIP('SRR','None',#32716,#188);
#188=ADVANCED_BREP_SHAPE_REPRESENTATION('',(#224),#32617);
#206=STYLED_ITEM('',(#32809),#224);
#224=MANIFOLD_SOLID_BREP('Body1',#8683);
#264=FACE_BOUND('',#1265,.T.);
#265=FACE_BOUND('',#1268,.T.);
#303=B_SPLINE_SURFACE_WITH_KNOTS('',3,3,((#25336,#25337,#25338,#25339,#25340,
#25341,#25342,#25343,#25344,#25345,#25346,#25347,#25348,#25349,#25350,#25351,
#25352,#25353,#25354,#25355,#25356,#25357,#25358,#25359,#25360,#25361,#25362,
#25363,#25364,#25365,#25366,#25367,#25368,#25369,#25370,#25371,#25372,#25373,
#25374,#25375,#25376,#25377,#25378,#25379,#25380,#25381,#25382,#25383,#25384,
#25385,#25386,#25387,#25388,#25389,#25390,#25391,#25392,#25393,#25394,#25395,
#25396,#25397,#25398,#25399,#25400,#25401,#25402,#25403,#25404,#25405),
(#25406,#25407,#25408,#25409,#25410,#25411,#25412,#25413,#25414,#25415,
#25416,#25417,#25418,#25419,#25420,#25421,#25422,#25423,#25424,#25425,#25426,
#25427,#25428,#25429,#25430,#25431,#25432,#25433,#25434,#25435,#25436,#25437,
#25438,#25439,#25440,#25441,#25442,#25443,#25444,#25445,#25446,#25447,#25448,
#25449,#25450,#25451,#25452,#25453,#25454,#25455,#25456,#25457,#25458,#25459,
#25460,#25461,#25462,#25463,#25464,#25465,#25466,#25467,#25468,#25469,#25470,
#25471,#25472,#25473,#25474,#25475),(#25476,#25477,#25478,#25479,#25480,
#25481,#25482,#25483,#25484,#25485,#25486,#25487,#25488,#25489,#25490,#25491,
#25492,#25493,#25494,#25495,#25496,#25497,#25498,#25499,#25500,#25501,#25502,
#25503,#25504,#25505,#25506,#25507,#25508,#25509,#25510,#25511,#25512,#25513,
#25514,#25515,#25516,#25517,#25518,#25519,#25520,#25521,#25522,#25523,#25524,
#25525,#25526,#25527,#25528,#25529,#25530,#25531,#25532,#25533,#25534,#25535,
#25536,#25537,#25538,#25539,#25540,#25541,#25542,#25543,#25544,#25545),
(#25546,#25547,#25548,#25549,#25550,#25551,#25552,#25553,#25554,#25555,
#25556,#25557,#25558,#25559,#25560,#25561,#25562,#25563,#25564,#25565,#25566,
#25567,#25568,#25569,#25570,#25571,#25572,#25573,#25574,#25575,#25576,#25577,
#25578,#25579,#25580,#25581,#25582,#25583,#25584,#25585,#25586,#25587,#25588,
#25589,#25590,#25591,#25592,#25593,#25594,#25595,#25596,#25597,#25598,#25599,
#25600,#25601,#25602,#25603,#25604,#25605,#25606,#25607,#25608,#25609,#25610,
#25611,#25612,#25613,#25614,#25615)),.UNSPECIFIED.,.F.,.F.,.F.,(4,4),(4,
1,1,1,1,1,1,1,1,1,1,1,1,1,1,1,1,1,1,1,1,1,1,1,1,1,1,1,1,1,1,1,1,1,1,1,1,
1,1,1,1,1,1,1,1,1,1,1,1,1,1,1,1,1,1,1,1,1,1,1,1,1,1,1,1,1,1,4),(0.,0.0460148164544132),
(11.6154215191106,12.6127599630189,13.6100984069272,14.6074368508354,15.6047752947437,
16.602113738652,17.5994521825603,18.5967906264686,19.5941290703769,20.5914675142851,
21.5888059581934,22.5861444021017,23.58348284601,24.5808212899183,25.5781597338266,
26.5754981777348,27.5728366216431,28.5701750655514,29.5675135094597,30.564851953368,
31.5621903972762,32.5595288411845,33.5568672850928,34.5542057290011,35.5515441729094,
36.5488826168177,37.5462210607259,38.5435595046342,39.5408979485425,40.5382363924508,
41.5355748363591,42.5329132802674,43.5302517241756,44.5275901680839,45.5249286119922,
46.5222670559005,47.5196054998088,48.516943943717,49.5142823876253,50.5116208315336,
51.5089592754419,52.5062977193502,53.5036361632585,54.5009746071667,55.498313051075,
56.4956514949833,57.4929899388916,58.4903283827999,59.4876668267081,60.4850052706164,
61.4823437145247,62.479682158433,63.4770206023413,64.4743590462496,65.4716974901578,
66.4690359340661,67.4663743779744,68.4637128218827,69.461051265791,70.4583897096992,
71.4557281536075,72.4530665975158,73.4504050414241,74.4477434853324,75.4450819292407,
76.4424203731489,77.4397588170572,78.4370972609655),.UNSPECIFIED.);
#304=B_SPLINE_SURFACE_WITH_KNOTS('',3,3,((#25741,#25742,#25743,#25744,#25745,
#25746,#25747,#25748,#25749,#25750,#25751,#25752,#25753,#25754,#25755,#25756,
#25757,#25758,#25759,#25760,#25761,#25762,#25763,#25764,#25765,#25766,#25767,
#25768,#25769,#25770,#25771,#25772,#25773,#25774,#25775,#25776,#25777,#25778,
#25779,#25780,#25781,#25782,#25783,#25784,#25785,#25786,#25787,#25788,#25789,
#25790,#25791,#25792,#25793,#25794,#25795,#25796,#25797,#25798,#25799,#25800,
#25801,#25802,#25803,#25804,#25805,#25806,#25807,#25808,#25809,#25810,#25811,
#25812),(#25813,#25814,#25815,#25816,#25817,#25818,#25819,#25820,#25821,
#25822,#25823,#25824,#25825,#25826,#25827,#25828,#25829,#25830,#25831,#25832,
#25833,#25834,#25835,#25836,#25837,#25838,#25839,#25840,#25841,#25842,#25843,
#25844,#25845,#25846,#25847,#25848,#25849,#25850,#25851,#25852,#25853,#25854,
#25855,#25856,#25857,#25858,#25859,#25860,#25861,#25862,#25863,#25864,#25865,
#25866,#25867,#25868,#25869,#25870,#25871,#25872,#25873,#25874,#25875,#25876,
#25877,#25878,#25879,#25880,#25881,#25882,#25883,#25884),(#25885,#25886,
#25887,#25888,#25889,#25890,#25891,#25892,#25893,#25894,#25895,#25896,#25897,
#25898,#25899,#25900,#25901,#25902,#25903,#25904,#25905,#25906,#25907,#25908,
#25909,#25910,#25911,#25912,#25913,#25914,#25915,#25916,#25917,#25918,#25919,
#25920,#25921,#25922,#25923,#25924,#25925,#25926,#25927,#25928,#25929,#25930,
#25931,#25932,#25933,#25934,#25935,#25936,#25937,#25938,#25939,#25940,#25941,
#25942,#25943,#25944,#25945,#25946,#25947,#25948,#25949,#25950,#25951,#25952,
#25953,#25954,#25955,#25956),(#25957,#25958,#25959,#25960,#25961,#25962,
#25963,#25964,#25965,#25966,#25967,#25968,#25969,#25970,#25971,#25972,#25973,
#25974,#25975,#25976,#25977,#25978,#25979,#25980,#25981,#25982,#25983,#25984,
#25985,#25986,#25987,#25988,#25989,#25990,#25991,#25992,#25993,#25994,#25995,
#25996,#25997,#25998,#25999,#26000,#26001,#26002,#26003,#26004,#26005,#26006,
#26007,#26008,#26009,#26010,#26011,#26012,#26013,#26014,#26015,#26016,#26017,
#26018,#26019,#26020,#26021,#26022,#26023,#26024,#26025,#26026,#26027,#26028)),
 .UNSPECIFIED.,.F.,.F.,.F.,(4,4),(4,1,1,1,1,1,1,1,1,1,1,1,1,1,1,1,1,1,1,
1,1,1,1,1,1,1,1,1,1,1,1,1,1,1,1,1,1,1,1,1,1,1,1,1,1,1,1,1,1,1,1,1,1,1,1,
1,1,1,1,1,1,1,1,1,1,1,1,1,1,4),(0.,0.0460148164544132),(8.31058692273974,
9.30894657310399,10.3073062234682,11.3056658738325,12.3040255241967,13.302385174561,
14.3007448249252,15.2991044752895,16.2974641256537,17.295823776018,18.2941834263822,
19.2925430767465,20.2909027271107,21.289262377475,22.2876220278392,23.2859816782034,
24.2843413285677,25.2827009789319,26.2810606292962,27.2794202796604,28.2777799300247,
29.2761395803889,30.2744992307532,31.2728588811174,32.2712185314817,33.2695781818459,
34.2679378322102,35.2662974825744,36.2646571329387,37.2630167833029,38.2613764336672,
39.2597360840314,40.2580957343957,41.2564553847599,42.2548150351241,43.2531746854884,
44.2515343358526,45.2498939862169,46.2482536365811,47.2466132869454,48.2449729373096,
49.2433325876739,50.2416922380381,51.2400518884024,52.2384115387666,53.2367711891309,
54.2351308394951,55.2334904898594,56.2318501402236,57.2302097905879,58.2285694409521,
59.2269290913164,60.2252887416806,61.2236483920448,62.2220080424091,63.2203676927733,
64.2187273431376,65.2170869935018,66.2154466438661,67.2138062942303,68.2121659445946,
69.2105255949588,70.2088852453231,71.2072448956873,72.2056045460516,73.2039641964158,
74.2023238467801,75.2006834971443,76.1990431475085,77.1974027978728),
 .UNSPECIFIED.);
#384=PLANE('',#9254);
#385=PLANE('',#9255);
#386=PLANE('',#9256);
#387=PLANE('',#9257);
#388=PLANE('',#9258);
#389=PLANE('',#9259);
#390=PLANE('',#9260);
#391=PLANE('',#9261);
#392=PLANE('',#9265);
#393=PLANE('',#9266);
#727=FACE_OUTER_BOUND('',#1232,.T.);
#728=FACE_OUTER_BOUND('',#1233,.T.);
#729=FACE_OUTER_BOUND('',#1234,.T.);
#730=FACE_OUTER_BOUND('',#1235,.T.);
#731=FACE_OUTER_BOUND('',#1236,.T.);
#732=FACE_OUTER_BOUND('',#1237,.T.);
#733=FACE_OUTER_BOUND('',#1238,.T.);
#734=FACE_OUTER_BOUND('',#1239,.T.);
#735=FACE_OUTER_BOUND('',#1240,.T.);
#736=FACE_OUTER_BOUND('',#1241,.T.);
#737=FACE_OUTER_BOUND('',#1242,.T.);
#738=FACE_OUTER_BOUND('',#1243,.T.);
#739=FACE_OUTER_BOUND('',#1244,.T.);
#740=FACE_OUTER_BOUND('',#1245,.T.);
#741=FACE_OUTER_BOUND('',#1246,.T.);
#742=FACE_OUTER_BOUND('',#1247,.T.);
#743=FACE_OUTER_BOUND('',#1248,.T.);
#744=FACE_OUTER_BOUND('',#1249,.T.);
#745=FACE_OUTER_BOUND('',#1250,.T.);
#746=FACE_OUTER_BOUND('',#1251,.T.);
#747=FACE_OUTER_BOUND('',#1252,.T.);
#748=FACE_OUTER_BOUND('',#1253,.T.);
#749=FACE_OUTER_BOUND('',#1254,.T.);
#750=FACE_OUTER_BOUND('',#1255,.T.);
#751=FACE_OUTER_BOUND('',#1256,.T.);
#752=FACE_OUTER_BOUND('',#1257,.T.);
#753=FACE_OUTER_BOUND('',#1258,.T.);
#754=FACE_OUTER_BOUND('',#1259,.T.);
#755=FACE_OUTER_BOUND('',#1260,.T.);
#756=FACE_OUTER_BOUND('',#1261,.T.);
#757=FACE_OUTER_BOUND('',#1262,.T.);
#758=FACE_OUTER_BOUND('',#1263,.T.);
#759=FACE_OUTER_BOUND('',#1264,.T.);
#760=FACE_OUTER_BOUND('',#1266,.T.);
#761=FACE_OUTER_BOUND('',#1267,.T.);
#762=FACE_OUTER_BOUND('',#1269,.T.);
#1232=EDGE_LOOP('',(#6861,#6862,#6863,#6864));
#1233=EDGE_LOOP('',(#6865,#6866,#6867,#6868));
#1234=EDGE_LOOP('',(#6869,#6870,#6871,#6872));
#1235=EDGE_LOOP('',(#6873,#6874,#6875,#6876));
#1236=EDGE_LOOP('',(#6877,#6878,#6879,#6880));
#1237=EDGE_LOOP('',(#6881,#6882,#6883,#6884));
#1238=EDGE_LOOP('',(#6885,#6886,#6887,#6888));
#1239=EDGE_LOOP('',(#6889,#6890,#6891,#6892));
#1240=EDGE_LOOP('',(#6893,#6894,#6895,#6896));
#1241=EDGE_LOOP('',(#6897,#6898,#6899,#6900));
#1242=EDGE_LOOP('',(#6901,#6902,#6903,#6904));
#1243=EDGE_LOOP('',(#6905,#6906,#6907,#6908));
#1244=EDGE_LOOP('',(#6909,#6910,#6911,#6912));
#1245=EDGE_LOOP('',(#6913,#6914,#6915,#6916));
#1246=EDGE_LOOP('',(#6917,#6918,#6919,#6920));
#1247=EDGE_LOOP('',(#6921,#6922,#6923,#6924));
#1248=EDGE_LOOP('',(#6925,#6926,#6927,#6928));
#1249=EDGE_LOOP('',(#6929,#6930,#6931,#6932));
#1250=EDGE_LOOP('',(#6933,#6934,#6935,#6936));
#1251=EDGE_LOOP('',(#6937,#6938,#6939,#6940));
#1252=EDGE_LOOP('',(#6941,#6942,#6943,#6944,#6945,#6946,#6947,#6948));
#1253=EDGE_LOOP('',(#6949,#6950,#6951,#6952,#6953,#6954,#6955,#6956,#6957,
#6958,#6959,#6960,#6961,#6962,#6963,#6964,#6965,#6966,#6967,#6968,#6969,
#6970,#6971,#6972));
#1254=EDGE_LOOP('',(#6973,#6974,#6975,#6976));
#1255=EDGE_LOOP('',(#6977,#6978,#6979,#6980,#6981,#6982,#6983,#6984,#6985,
#6986,#6987,#6988,#6989,#6990,#6991,#6992,#6993,#6994,#6995,#6996,#6997,
#6998,#6999,#7000,#7001));
#1256=EDGE_LOOP('',(#7002,#7003,#7004,#7005));
#1257=EDGE_LOOP('',(#7006,#7007,#7008,#7009));
#1258=EDGE_LOOP('',(#7010,#7011,#7012,#7013));
#1259=EDGE_LOOP('',(#7014,#7015,#7016,#7017));
#1260=EDGE_LOOP('',(#7018,#7019,#7020,#7021));
#1261=EDGE_LOOP('',(#7022,#7023,#7024,#7025));
#1262=EDGE_LOOP('',(#7026,#7027,#7028,#7029));
#1263=EDGE_LOOP('',(#7030,#7031,#7032,#7033,#7034,#7035));
#1264=EDGE_LOOP('',(#7036));
#1265=EDGE_LOOP('',(#7037,#7038,#7039,#7040));
#1266=EDGE_LOOP('',(#7041,#7042,#7043,#7044));
#1267=EDGE_LOOP('',(#7045));
#1268=EDGE_LOOP('',(#7046,#7047,#7048,#7049,#7050,#7051));
#1269=EDGE_LOOP('',(#7052));
#1520=CIRCLE('',#9227,1.954);
#1521=CIRCLE('',#9238,1.5555);
#1522=CIRCLE('',#9249,1.954);
#1523=CIRCLE('',#9250,1.);
#1524=CIRCLE('',#9252,1.5555);
#1525=CIRCLE('',#9262,3.5);
#1526=CIRCLE('',#9264,3.5);
#1960=B_SPLINE_CURVE_WITH_KNOTS('',3,(#24328,#24329,#24330,#24331,#24332,
#24333,#24334,#24335,#24336,#24337),.UNSPECIFIED.,.F.,.F.,(4,3,3,4),(-4.09254174883832,
-3.98935377563313,-2.99201533172485,-2.06514013327812),.UNSPECIFIED.);
#1961=B_SPLINE_CURVE_WITH_KNOTS('',3,(#24340,#24341,#24342,#24343,#24344,
#24345,#24346),.UNSPECIFIED.,.F.,.F.,(4,3,4),(0.,0.998359650364244,1.11419103802955),
 .UNSPECIFIED.);
#1962=B_SPLINE_CURVE_WITH_KNOTS('',3,(#24351,#24352,#24353,#24354,#24355,
#24356,#24357,#24358,#24359,#24360,#24361,#24362,#24363,#24364,#24365,#24366,
#24367,#24368,#24369,#24370,#24371,#24372),.UNSPECIFIED.,.F.,.F.,(4,3,3,
3,3,3,3,4),(-10.3757270560179,-9.97338443908282,-8.97604599517454,-7.97870755126626,
-6.98136910735798,-5.98403066344969,-4.98669221954141,-4.09254174883832),
 .UNSPECIFIED.);
#1963=B_SPLINE_CURVE_WITH_KNOTS('',3,(#24373,#24374,#24375,#24376,#24377,
#24378,#24379,#24380,#24381,#24382,#24383,#24384,#24385,#24386,#24387,#24388,
#24389,#24390,#24391,#24392,#24393,#24394),.UNSPECIFIED.,.F.,.F.,(4,3,3,
3,3,3,3,4),(1.11419103802955,1.99671930072849,2.99507895109274,3.99343860145699,
4.99179825182123,5.99015790218548,6.98851755254973,7.39737634520914),
 .UNSPECIFIED.);
#1964=B_SPLINE_CURVE_WITH_KNOTS('',3,(#24399,#24400,#24401,#24402,#24403,
#24404,#24405,#24406,#24407,#24408,#24409,#24410,#24411,#24412,#24413,#24414,
#24415,#24416,#24417,#24418,#24419,#24420),.UNSPECIFIED.,.F.,.F.,(4,3,3,
3,3,3,3,4),(-16.6589123631975,-15.9574151025325,-14.9600766586242,-13.962738214716,
-12.9653997708077,-11.9680613268994,-10.9707228829911,-10.3757270560179),
 .UNSPECIFIED.);
#1965=B_SPLINE_CURVE_WITH_KNOTS('',3,(#24421,#24422,#24423,#24424,#24425,
#24426,#24427,#24428,#24429,#24430,#24431,#24432,#24433,#24434,#24435,#24436,
#24437,#24438,#24439,#24440,#24441,#24442),.UNSPECIFIED.,.F.,.F.,(4,3,3,
3,3,3,3,4),(7.39737634520914,7.98687720291397,8.98523685327822,9.98359650364247,
10.9819561540067,11.980315804371,12.9786754547352,13.6805616523887),
 .UNSPECIFIED.);
#1966=B_SPLINE_CURVE_WITH_KNOTS('',3,(#24447,#24448,#24449,#24450,#24451,
#24452,#24453,#24454,#24455,#24456,#24457,#24458,#24459,#24460,#24461,#24462,
#24463,#24464,#24465,#24466,#24467,#24468,#24469,#24470,#24471),
 .UNSPECIFIED.,.F.,.F.,(4,3,3,3,3,3,3,3,4),(-22.9420976703771,-22.9387842098905,
-21.9414457659822,-20.9441073220739,-19.9467688781656,-18.9494304342574,
-17.9520919903491,-16.9547535464408,-16.6589123631975),.UNSPECIFIED.);
#1967=B_SPLINE_CURVE_WITH_KNOTS('',3,(#24472,#24473,#24474,#24475,#24476,
#24477,#24478,#24479,#24480,#24481,#24482,#24483,#24484,#24485,#24486,#24487,
#24488,#24489,#24490,#24491,#24492,#24493),.UNSPECIFIED.,.F.,.F.,(4,3,3,
3,3,3,3,4),(13.6805616523887,13.9770351050995,14.9753947554637,15.973754405828,
16.9721140561922,17.9704737065565,18.9688333569207,19.9637469595683),
 .UNSPECIFIED.);
#1968=B_SPLINE_CURVE_WITH_KNOTS('',3,(#24498,#24499,#24500,#24501,#24502,
#24503,#24504,#24505,#24506,#24507,#24508,#24509,#24510,#24511,#24512,#24513,
#24514,#24515,#24516,#24517,#24518,#24519),.UNSPECIFIED.,.F.,.F.,(4,3,3,
3,3,3,3,4),(-29.2252829775567,-28.9228148733402,-27.9254764294319,-26.9281379855236,
-25.9307995416153,-24.9334610977071,-23.9361226537988,-22.9420976703771),
 .UNSPECIFIED.);
#1969=B_SPLINE_CURVE_WITH_KNOTS('',3,(#24520,#24521,#24522,#24523,#24524,
#24525,#24526,#24527,#24528,#24529,#24530,#24531,#24532,#24533,#24534,#24535,
#24536,#24537,#24538,#24539,#24540,#24541,#24542,#24543,#24544),
 .UNSPECIFIED.,.F.,.F.,(4,3,3,3,3,3,3,3,4),(19.9637469595683,19.967193007285,
20.9655526576492,21.9639123080134,22.9622719583777,23.9606316087419,24.9589912591062,
25.9573509094704,26.2469322667479),.UNSPECIFIED.);
#1970=B_SPLINE_CURVE_WITH_KNOTS('',3,(#24549,#24550,#24551,#24552,#24553,
#24554,#24555,#24556,#24557,#24558,#24559,#24560,#24561,#24562,#24563,#24564,
#24565,#24566,#24567,#24568,#24569,#24570),.UNSPECIFIED.,.F.,.F.,(4,3,3,
3,3,3,3,4),(-35.5084682847363,-34.9068455367899,-33.9095070928816,-32.9121686489733,
-31.914830205065,-30.9174917611567,-29.9201533172485,-29.2252829775567),
 .UNSPECIFIED.);
#1971=B_SPLINE_CURVE_WITH_KNOTS('',3,(#24571,#24572,#24573,#24574,#24575,
#24576,#24577,#24578,#24579,#24580,#24581,#24582,#24583,#24584,#24585,#24586,
#24587,#24588,#24589,#24590,#24591,#24592),.UNSPECIFIED.,.F.,.F.,(4,3,3,
3,3,3,3,4),(26.2469322667479,26.9557105598347,27.9540702101989,28.9524298605632,
29.9507895109274,30.9491491612917,31.9475088116559,32.5301175739275),
 .UNSPECIFIED.);
#1972=B_SPLINE_CURVE_WITH_KNOTS('',3,(#24597,#24598,#24599,#24600,#24601,
#24602,#24603,#24604,#24605,#24606,#24607,#24608,#24609,#24610,#24611,#24612,
#24613,#24614,#24615,#24616,#24617,#24618),.UNSPECIFIED.,.F.,.F.,(4,3,3,
3,3,3,3,4),(-41.7916535919158,-40.8908762002396,-39.8935377563313,-38.896199312423,
-37.8988608685147,-36.9015224246064,-35.9041839806982,-35.5084682847363),
 .UNSPECIFIED.);
#1973=B_SPLINE_CURVE_WITH_KNOTS('',3,(#24619,#24620,#24621,#24622,#24623,
#24624,#24625,#24626,#24627,#24628,#24629,#24630,#24631,#24632,#24633,#24634,
#24635,#24636,#24637,#24638,#24639,#24640),.UNSPECIFIED.,.F.,.F.,(4,3,3,
3,3,3,3,4),(32.5301175739275,32.9458684620202,33.9442281123844,34.9425877627486,
35.9409474131129,36.9393070634771,37.9376667138414,38.8133028811071),
 .UNSPECIFIED.);
#1974=B_SPLINE_CURVE_WITH_KNOTS('',3,(#24645,#24646,#24647,#24648,#24649,
#24650,#24651,#24652,#24653,#24654,#24655,#24656,#24657,#24658,#24659,#24660,
#24661,#24662,#24663,#24664,#24665,#24666,#24667,#24668,#24669),
 .UNSPECIFIED.,.F.,.F.,(4,3,3,3,3,3,3,3,4),(-48.0748388990954,-47.8722453075976,
-46.8749068636893,-45.877568419781,-44.8802299758727,-43.8828915319644,
-42.8855530880561,-41.8882146441479,-41.7916535919158),.UNSPECIFIED.);
#1975=B_SPLINE_CURVE_WITH_KNOTS('',3,(#24670,#24671,#24672,#24673,#24674,
#24675,#24676,#24677,#24678,#24679,#24680,#24681,#24682,#24683,#24684,#24685,
#24686,#24687,#24688,#24689,#24690,#24691,#24692,#24693,#24694),
 .UNSPECIFIED.,.F.,.F.,(4,3,3,3,3,3,3,3,4),(38.8133028811071,38.9360263642056,
39.9343860145699,40.9327456649341,41.9311053152984,42.9294649656626,43.9278246160269,
44.9261842663911,45.0964881882867),.UNSPECIFIED.);
#1976=B_SPLINE_CURVE_WITH_KNOTS('',3,(#24699,#24700,#24701,#24702,#24703,
#24704,#24705,#24706,#24707,#24708,#24709,#24710,#24711,#24712,#24713,#24714,
#24715,#24716,#24717,#24718,#24719,#24720),.UNSPECIFIED.,.F.,.F.,(4,3,3,
3,3,3,3,4),(-54.358024206275,-53.8562759710472,-52.858937527139,-51.8615990832307,
-50.8642606393224,-49.8669221954141,-48.8695837515058,-48.0748388990954),
 .UNSPECIFIED.);
#1977=B_SPLINE_CURVE_WITH_KNOTS('',3,(#24721,#24722,#24723,#24724,#24725,
#24726,#24727,#24728,#24729,#24730,#24731,#24732,#24733,#24734,#24735,#24736,
#24737,#24738,#24739,#24740,#24741,#24742),.UNSPECIFIED.,.F.,.F.,(4,3,3,
3,3,3,3,4),(45.0964881882867,45.9245439167554,46.9229035671196,47.9212632174839,
48.9196228678481,49.9179825182124,50.9163421685766,51.3796734954663),
 .UNSPECIFIED.);
#1978=B_SPLINE_CURVE_WITH_KNOTS('',3,(#24747,#24748,#24749,#24750,#24751,
#24752,#24753,#24754,#24755,#24756,#24757,#24758,#24759,#24760,#24761,#24762,
#24763,#24764,#24765,#24766,#24767,#24768),.UNSPECIFIED.,.F.,.F.,(4,3,3,
3,3,3,3,4),(-60.6412095134546,-59.8403066344969,-58.8429681905886,-57.8456297466804,
-56.8482913027721,-55.8509528588638,-54.8536144149555,-54.358024206275),
 .UNSPECIFIED.);
#1979=B_SPLINE_CURVE_WITH_KNOTS('',3,(#24769,#24770,#24771,#24772,#24773,
#24774,#24775,#24776,#24777,#24778,#24779,#24780,#24781,#24782,#24783,#24784,
#24785,#24786,#24787,#24788,#24789,#24790),.UNSPECIFIED.,.F.,.F.,(4,3,3,
3,3,3,3,4),(51.3796734954663,51.9147018189409,52.9130614693051,53.9114211196693,
54.9097807700336,55.9081404203978,56.9065000707621,57.6628588026459),
 .UNSPECIFIED.);
#1980=B_SPLINE_CURVE_WITH_KNOTS('',3,(#24796,#24797,#24798,#24799,#24800,
#24801,#24802,#24803,#24804,#24805),.UNSPECIFIED.,.F.,.F.,(4,1,1,1,1,1,
1,4),(72.2566310325653,72.4530665975158,73.4504050414241,74.4477434853324,
75.4450819292407,76.4424203731489,77.4397588170572,78.4370972609655),
 .UNSPECIFIED.);
#1981=B_SPLINE_CURVE_WITH_KNOTS('',3,(#24808,#24809,#24810,#24811,#24812,
#24813,#24814,#24815),.UNSPECIFIED.,.F.,.F.,(4,1,1,1,1,4),(72.2566310325652,
73.2039641964158,74.2023238467801,75.2006834971443,76.1990431475085,77.1974027978728),
 .UNSPECIFIED.);
#1982=B_SPLINE_CURVE_WITH_KNOTS('',3,(#24820,#24821,#24822,#24823,#24824,
#24825,#24826,#24827,#24828,#24829),.UNSPECIFIED.,.F.,.F.,(4,1,1,1,1,1,
1,4),(65.9734457253856,66.4690359340661,67.4663743779744,68.4637128218827,
69.461051265791,70.4583897096992,71.4557281536075,72.2566310325653),
 .UNSPECIFIED.);
#1983=B_SPLINE_CURVE_WITH_KNOTS('',3,(#24830,#24831,#24832,#24833,#24834,
#24835,#24836,#24837,#24838,#24839,#24840),.UNSPECIFIED.,.F.,.F.,(4,1,1,
1,1,1,1,1,4),(65.9734457253856,66.2154466438661,67.2138062942303,68.2121659445946,
69.2105255949588,70.2088852453231,71.2072448956873,72.2056045460516,72.2566310325652),
 .UNSPECIFIED.);
#1984=B_SPLINE_CURVE_WITH_KNOTS('',3,(#24845,#24846,#24847,#24848,#24849,
#24850,#24851,#24852,#24853,#24854),.UNSPECIFIED.,.F.,.F.,(4,1,1,1,1,1,
1,4),(59.6902604182061,60.4850052706164,61.4823437145247,62.479682158433,
63.4770206023413,64.4743590462496,65.4716974901578,65.9734457253856),
 .UNSPECIFIED.);
#1985=B_SPLINE_CURVE_WITH_KNOTS('',3,(#24855,#24856,#24857,#24858,#24859,
#24860,#24861,#24862,#24863,#24864),.UNSPECIFIED.,.F.,.F.,(4,1,1,1,1,1,
1,4),(59.6902604182061,60.2252887416806,61.2236483920448,62.2220080424091,
63.2203676927733,64.2187273431376,65.2170869935018,65.9734457253856),
 .UNSPECIFIED.);
#1986=B_SPLINE_CURVE_WITH_KNOTS('',3,(#24869,#24870,#24871,#24872,#24873,
#24874,#24875,#24876,#24877,#24878,#24879),.UNSPECIFIED.,.F.,.F.,(4,1,1,
1,1,1,1,1,4),(53.4070751110265,53.5036361632585,54.5009746071667,55.498313051075,
56.4956514949833,57.4929899388916,58.4903283827999,59.4876668267081,59.6902604182061),
 .UNSPECIFIED.);
#1987=B_SPLINE_CURVE_WITH_KNOTS('',3,(#24880,#24881,#24882,#24883,#24884,
#24885,#24886,#24887,#24888,#24889),.UNSPECIFIED.,.F.,.F.,(4,1,1,1,1,1,
1,4),(53.4070751110265,54.2351308394951,55.2334904898594,56.2318501402236,
57.2302097905879,58.2285694409521,59.2269290913164,59.6902604182061),
 .UNSPECIFIED.);
#1988=B_SPLINE_CURVE_WITH_KNOTS('',3,(#24894,#24895,#24896,#24897,#24898,
#24899,#24900,#24901,#24902,#24903),.UNSPECIFIED.,.F.,.F.,(4,1,1,1,1,1,
1,4),(47.1238898038469,47.5196054998088,48.516943943717,49.5142823876253,
50.5116208315336,51.5089592754419,52.5062977193502,53.4070751110265),
 .UNSPECIFIED.);
#1989=B_SPLINE_CURVE_WITH_KNOTS('',3,(#24904,#24905,#24906,#24907,#24908,
#24909,#24910,#24911,#24912,#24913,#24914),.UNSPECIFIED.,.F.,.F.,(4,1,1,
1,1,1,1,1,4),(47.1238898038469,47.2466132869454,48.2449729373096,49.2433325876739,
50.2416922380381,51.2400518884024,52.2384115387666,53.2367711891309,53.4070751110265),
 .UNSPECIFIED.);
#1990=B_SPLINE_CURVE_WITH_KNOTS('',3,(#24919,#24920,#24921,#24922,#24923,
#24924,#24925,#24926,#24927,#24928),.UNSPECIFIED.,.F.,.F.,(4,1,1,1,1,1,
1,4),(40.8407044966673,41.5355748363591,42.5329132802674,43.5302517241756,
44.5275901680839,45.5249286119922,46.5222670559005,47.1238898038469),
 .UNSPECIFIED.);
#1991=B_SPLINE_CURVE_WITH_KNOTS('',3,(#24929,#24930,#24931,#24932,#24933,
#24934,#24935,#24936,#24937,#24938),.UNSPECIFIED.,.F.,.F.,(4,1,1,1,1,1,
1,4),(40.8407044966673,41.2564553847599,42.2548150351241,43.2531746854884,
44.2515343358526,45.2498939862169,46.2482536365811,47.1238898038469),
 .UNSPECIFIED.);
#1992=B_SPLINE_CURVE_WITH_KNOTS('',3,(#24943,#24944,#24945,#24946,#24947,
#24948,#24949,#24950,#24951,#24952),.UNSPECIFIED.,.F.,.F.,(4,1,1,1,1,1,
1,4),(34.5575191894877,35.5515441729094,36.5488826168177,37.5462210607259,
38.5435595046342,39.5408979485425,40.5382363924508,40.8407044966673),
 .UNSPECIFIED.);
#1993=B_SPLINE_CURVE_WITH_KNOTS('',3,(#24953,#24954,#24955,#24956,#24957,
#24958,#24959,#24960,#24961,#24962),.UNSPECIFIED.,.F.,.F.,(4,1,1,1,1,1,
1,4),(34.5575191894877,35.2662974825744,36.2646571329387,37.2630167833029,
38.2613764336672,39.2597360840314,40.2580957343957,40.8407044966673),
 .UNSPECIFIED.);
#1994=B_SPLINE_CURVE_WITH_KNOTS('',3,(#24967,#24968,#24969,#24970,#24971,
#24972,#24973,#24974,#24975,#24976,#24977),.UNSPECIFIED.,.F.,.F.,(4,1,1,
1,1,1,1,1,4),(28.2743338823081,28.5701750655514,29.5675135094597,30.564851953368,
31.5621903972762,32.5595288411845,33.5568672850928,34.5542057290011,34.5575191894877),
 .UNSPECIFIED.);
#1995=B_SPLINE_CURVE_WITH_KNOTS('',3,(#24978,#24979,#24980,#24981,#24982,
#24983,#24984,#24985,#24986,#24987,#24988),.UNSPECIFIED.,.F.,.F.,(4,1,1,
1,1,1,1,1,4),(28.2743338823081,28.2777799300247,29.2761395803889,30.2744992307532,
31.2728588811174,32.2712185314817,33.2695781818459,34.2679378322102,34.5575191894877),
 .UNSPECIFIED.);
#1996=B_SPLINE_CURVE_WITH_KNOTS('',3,(#24993,#24994,#24995,#24996,#24997,
#24998,#24999,#25000,#25001,#25002),.UNSPECIFIED.,.F.,.F.,(4,1,1,1,1,1,
1,4),(21.9911485751285,22.5861444021017,23.58348284601,24.5808212899183,
25.5781597338266,26.5754981777348,27.5728366216431,28.2743338823081),
 .UNSPECIFIED.);
#1997=B_SPLINE_CURVE_WITH_KNOTS('',3,(#25003,#25004,#25005,#25006,#25007,
#25008,#25009,#25010,#25011,#25012),.UNSPECIFIED.,.F.,.F.,(4,1,1,1,1,1,
1,4),(21.9911485751285,22.2876220278392,23.2859816782034,24.2843413285677,
25.2827009789319,26.2810606292962,27.2794202796604,28.2743338823081),
 .UNSPECIFIED.);
#1998=B_SPLINE_CURVE_WITH_KNOTS('',3,(#25017,#25018,#25019,#25020,#25021,
#25022,#25023,#25024,#25025,#25026),.UNSPECIFIED.,.F.,.F.,(4,1,1,1,1,1,
1,4),(15.7079632679489,16.602113738652,17.5994521825603,18.5967906264686,
19.5941290703769,20.5914675142851,21.5888059581934,21.9911485751285),
 .UNSPECIFIED.);
#1999=B_SPLINE_CURVE_WITH_KNOTS('',3,(#25027,#25028,#25029,#25030,#25031,
#25032,#25033,#25034,#25035,#25036),.UNSPECIFIED.,.F.,.F.,(4,1,1,1,1,1,
1,4),(15.7079632679489,16.2974641256537,17.295823776018,18.2941834263822,
19.2925430767465,20.2909027271107,21.289262377475,21.9911485751285),
 .UNSPECIFIED.);
#2000=B_SPLINE_CURVE_WITH_KNOTS('',3,(#25039,#25040,#25041,#25042,#25043,
#25044,#25045,#25046,#25047,#25048,#25049,#25050,#25051,#25052,#25053,#25054,
#25055,#25056,#25057,#25058,#25059,#25060,#25061,#25062,#25063,#25064,#25065,
#25066,#25067,#25068,#25069,#25070,#25071,#25072,#25073,#25074,#25075,#25076,
#25077,#25078,#25079,#25080,#25081,#25082,#25083,#25084,#25085,#25086,#25087,
#25088,#25089,#25090,#25091,#25092,#25093,#25094,#25095,#25096,#25097,#25098,
#25099,#25100,#25101,#25102,#25103,#25104,#25105,#25106,#25107,#25108,#25109,
#25110,#25111,#25112,#25113,#25114,#25115,#25116,#25117,#25118,#25119,#25120,
#25121,#25122,#25123,#25124,#25125,#25126,#25127,#25128,#25129,#25130,#25131,
#25132,#25133,#25134,#25135,#25136,#25137,#25138,#25139,#25140,#25141,#25142,
#25143,#25144,#25145,#25146,#25147,#25148,#25149,#25150,#25151,#25152,#25153,
#25154,#25155,#25156,#25157,#25158,#25159,#25160,#25161,#25162,#25163,#25164,
#25165,#25166,#25167,#25168,#25169,#25170,#25171,#25172,#25173,#25174,#25175,
#25176,#25177,#25178,#25179,#25180,#25181,#25182,#25183,#25184,#25185,#25186,
#25187,#25188,#25189,#25190,#25191,#25192,#25193,#25194,#25195,#25196,#25197,
#25198,#25199,#25200,#25201,#25202,#25203,#25204,#25205,#25206,#25207,#25208,
#25209,#25210,#25211,#25212,#25213,#25214,#25215,#25216,#25217,#25218,#25219,
#25220,#25221,#25222,#25223,#25224,#25225,#25226,#25227,#25228,#25229,#25230,
#25231,#25232,#25233,#25234,#25235,#25236,#25237,#25238,#25239,#25240,#25241,
#25242,#25243),.UNSPECIFIED.,.F.,.F.,(4,3,3,3,3,3,3,3,3,3,3,3,3,3,3,3,3,
3,3,3,3,3,3,3,3,3,3,3,3,3,3,3,3,3,3,3,3,3,3,3,3,3,3,3,3,3,3,3,3,3,3,3,3,
3,3,3,3,3,3,3,3,3,3,3,3,3,3,3,4),(-0.996917990983889,-0.978871820698626,
-0.961104366684017,-0.951552920986235,-0.947856438601261,-0.928927311919591,
-0.909844934708151,-0.904827747876617,-0.901690020918146,-0.882383426909664,
-0.863197144412726,-0.849964666497242,-0.841946217765742,-0.838653066670214,
-0.836732188581758,-0.818195847210497,-0.79884286378821,-0.782668226932182,
-0.778162385717433,-0.774287931072979,-0.754720517493441,-0.734912656248282,
-0.718545934421209,-0.712508687338266,-0.709097549624951,-0.689177599037007,
-0.66944576893999,-0.649768871196005,-0.645300371314176,-0.641533261094732,
-0.621745212512907,-0.601563770435519,-0.588280416256018,-0.579851467607475,
-0.575105400436484,-0.55460765219522,-0.534203727151442,-0.514750332075477,
-0.510181591792683,-0.506682086087755,-0.495296936999511,-0.475415657124971,
-0.455258237398922,-0.446439366268775,-0.440745412953617,-0.437134753004049,
-0.41645257608894,-0.395479514073081,-0.375148710383956,-0.368821709024976,
-0.365366889657485,-0.344172462410384,-0.323356461419818,-0.31415629931658,
-0.303019600034791,-0.297245219492413,-0.293778204123757,-0.272935156968737,
-0.251638706464901,-0.237180007007782,-0.228159672465448,-0.224715742096491,
-0.221072456791868,-0.199410898099475,-0.17780203126093,-0.156885571034439,
-0.151911241963545,-0.148372189075213,-0.135969110807948),.UNSPECIFIED.);
#2001=B_SPLINE_CURVE_WITH_KNOTS('',3,(#25245,#25246,#25247,#25248,#25249,
#25250,#25251,#25252,#25253,#25254,#25255,#25256,#25257,#25258,#25259,#25260,
#25261,#25262,#25263,#25264,#25265,#25266,#25267,#25268,#25269,#25270,#25271,
#25272,#25273,#25274,#25275,#25276,#25277,#25278,#25279,#25280,#25281,#25282,
#25283,#25284,#25285,#25286,#25287,#25288,#25289,#25290,#25291,#25292,#25293,
#25294,#25295,#25296,#25297,#25298,#25299,#25300,#25301,#25302),
 .UNSPECIFIED.,.F.,.F.,(4,3,3,3,3,3,3,3,3,3,3,3,3,3,3,3,3,3,3,4),(-0.271362855059846,
-0.249815149227379,-0.228817911637578,-0.214757147690894,-0.202696405081427,
-0.199258885355278,-0.179079500439592,-0.172574855850844,-0.151002998869488,
-0.132127624010802,-0.128545226638174,-0.108660379749781,-0.0889046558653028,
-0.0695674270863146,-0.0643977980835871,-0.0611874131352371,-0.042433397437552,
-0.0240016538661123,-0.00610725636958426,0.),.UNSPECIFIED.);
#2002=B_SPLINE_CURVE_WITH_KNOTS('',3,(#25305,#25306,#25307,#25308,#25309,
#25310,#25311,#25312,#25313,#25314,#25315,#25316,#25317,#25318,#25319,#25320,
#25321,#25322,#25323,#25324,#25325,#25326,#25327,#25328,#25329,#25330,#25331,
#25332),.UNSPECIFIED.,.F.,.F.,(4,3,3,3,3,3,3,3,3,4),(-0.135969110807948,
-0.126188073854222,-0.104892740575823,-0.0831670570417323,-0.0779384685470277,
-0.0734086019617295,-0.0516285578143609,-0.0295399653803274,-0.00752416693119264,
0.),.UNSPECIFIED.);
#2003=B_SPLINE_CURVE_WITH_KNOTS('',3,(#25617,#25618,#25619,#25620,#25621,
#25622,#25623,#25624),.UNSPECIFIED.,.F.,.F.,(4,1,1,1,1,4),(11.6154215191106,
12.6127599630189,13.6100984069272,14.6074368508354,15.6047752947437,15.7079632679489),
 .UNSPECIFIED.);
#2004=B_SPLINE_CURVE_WITH_KNOTS('',3,(#25625,#25626,#25627,#25628,#25629,
#25630,#25631,#25632,#25633,#25634,#25635,#25636,#25637,#25638,#25639,#25640,
#25641,#25642,#25643,#25644,#25645,#25646,#25647,#25648,#25649,#25650,#25651,
#25652,#25653,#25654,#25655,#25656,#25657,#25658,#25659,#25660,#25661,#25662,
#25663,#25664,#25665,#25666,#25667,#25668,#25669,#25670,#25671,#25672,#25673,
#25674,#25675,#25676,#25677,#25678,#25679,#25680,#25681,#25682,#25683,#25684,
#25685,#25686,#25687,#25688,#25689,#25690,#25691,#25692,#25693,#25694,#25695,
#25696,#25697,#25698,#25699,#25700,#25701,#25702,#25703,#25704,#25705,#25706,
#25707,#25708,#25709),.UNSPECIFIED.,.F.,.F.,(4,3,3,3,3,3,3,3,3,3,3,3,3,
3,3,3,3,3,3,3,3,3,3,3,3,3,3,3,4),(-0.364629307890661,-0.350886771084415,
-0.329297510939725,-0.318979842765136,-0.313748856729508,-0.309367238941102,
-0.288044972781349,-0.272811108278258,-0.264009728102714,-0.260298972601032,
-0.239567880035138,-0.219347617431434,-0.206054227262732,-0.194878207820902,
-0.191399429390758,-0.17181371271556,-0.166174056756627,-0.145402299662048,
-0.12670765132229,-0.123381127587156,-0.103926762733045,-0.0845494608218094,
-0.0655688723802368,-0.0621691825638593,-0.0589309125894093,-0.0403408647045067,
-0.0220852216194749,-0.00441218938162483,0.),.UNSPECIFIED.);
#2005=B_SPLINE_CURVE_WITH_KNOTS('',3,(#25710,#25711,#25712,#25713,#25714,
#25715,#25716,#25717,#25718,#25719,#25720,#25721,#25722,#25723,#25724,#25725,
#25726,#25727,#25728),.UNSPECIFIED.,.F.,.F.,(4,3,3,3,3,3,4),(-65.3098882395457,
-64.8269988540384,-63.8296604101301,-62.8323219662218,-61.8349835223135,
-60.8376450784052,-60.6412095134546),.UNSPECIFIED.);
#2006=B_SPLINE_CURVE_WITH_KNOTS('',3,(#25731,#25732,#25733,#25734,#25735,
#25736,#25737,#25738,#25739),.UNSPECIFIED.,.F.,.F.,(4,1,1,1,1,1,4),(10.3757270560179,
11.3056658738325,12.3040255241967,13.302385174561,14.3007448249252,15.2991044752895,
15.7079632679489),.UNSPECIFIED.);
#2007=B_SPLINE_CURVE_WITH_KNOTS('',3,(#26029,#26030,#26031,#26032,#26033,
#26034,#26035,#26036,#26037,#26038,#26039,#26040,#26041,#26042,#26043,#26044,
#26045,#26046,#26047,#26048,#26049,#26050),.UNSPECIFIED.,.F.,.F.,(4,3,3,
3,3,3,3,4),(57.6628588026459,57.9048597211263,58.9032193714906,59.9015790218548,
60.8999386722191,61.8982983225833,62.8966579729476,63.2447481062677),
 .UNSPECIFIED.);
#2008=B_SPLINE_CURVE_WITH_KNOTS('',3,(#26051,#26052,#26053,#26054,#26055,
#26056,#26057,#26058,#26059,#26060,#26061,#26062,#26063,#26064,#26065,#26066,
#26067,#26068,#26069,#26070,#26071,#26072,#26073,#26074,#26075,#26076,#26077,
#26078,#26079,#26080,#26081,#26082,#26083,#26084,#26085,#26086,#26087,#26088,
#26089,#26090,#26091,#26092,#26093,#26094,#26095,#26096,#26097,#26098,#26099,
#26100,#26101,#26102,#26103,#26104,#26105,#26106,#26107,#26108,#26109,#26110,
#26111,#26112,#26113,#26114,#26115,#26116,#26117,#26118,#26119,#26120,#26121,
#26122,#26123,#26124,#26125,#26126,#26127,#26128,#26129,#26130,#26131,#26132),
 .UNSPECIFIED.,.F.,.F.,(4,3,3,3,3,3,3,3,3,3,3,3,3,3,3,3,3,3,3,3,3,3,3,3,
3,3,3,4),(-0.366397579005847,-0.355573362530754,-0.337605442405704,-0.327398200425482,
-0.321620335202968,-0.30281021010297,-0.288367976755365,-0.281197910953663,
-0.277581602535663,-0.258139779174731,-0.23832225991534,-0.225559780767037,
-0.21845666374658,-0.214865898441521,-0.194435927724086,-0.187272343322128,
-0.167568574984456,-0.146399230996079,-0.142991450501546,-0.122489503287978,
-0.101565610408655,-0.0804999660718792,-0.0757146540182571,-0.0722132271210984,
-0.0505693460362938,-0.0288755213118303,-0.00764564704115539,0.),
 .UNSPECIFIED.);
#2488=LINE('',#24326,#3034);
#2489=LINE('',#24350,#3035);
#2490=LINE('',#24398,#3036);
#2491=LINE('',#24446,#3037);
#2492=LINE('',#24497,#3038);
#2493=LINE('',#24548,#3039);
#2494=LINE('',#24596,#3040);
#2495=LINE('',#24644,#3041);
#2496=LINE('',#24698,#3042);
#2497=LINE('',#24746,#3043);
#2498=LINE('',#24794,#3044);
#2499=LINE('',#24819,#3045);
#2500=LINE('',#24844,#3046);
#2501=LINE('',#24868,#3047);
#2502=LINE('',#24893,#3048);
#2503=LINE('',#24918,#3049);
#2504=LINE('',#24942,#3050);
#2505=LINE('',#24966,#3051);
#2506=LINE('',#24992,#3052);
#2507=LINE('',#25016,#3053);
#2508=LINE('',#25334,#3054);
#2509=LINE('',#26137,#3055);
#2510=LINE('',#26139,#3056);
#2511=LINE('',#26141,#3057);
#2512=LINE('',#26142,#3058);
#2513=LINE('',#26145,#3059);
#2514=LINE('',#26147,#3060);
#2515=LINE('',#26148,#3061);
#2516=LINE('',#26151,#3062);
#2517=LINE('',#26153,#3063);
#2518=LINE('',#26154,#3064);
#2519=LINE('',#26157,#3065);
#2520=LINE('',#26159,#3066);
#2521=LINE('',#26160,#3067);
#2522=LINE('',#26163,#3068);
#2523=LINE('',#26165,#3069);
#2524=LINE('',#26166,#3070);
#2525=LINE('',#26168,#3071);
#2526=LINE('',#26169,#3072);
#2527=LINE('',#26176,#3073);
#3034=VECTOR('',#10512,2.);
#3035=VECTOR('',#10517,2.);
#3036=VECTOR('',#10520,2.);
#3037=VECTOR('',#10523,2.);
#3038=VECTOR('',#10526,2.);
#3039=VECTOR('',#10529,2.);
#3040=VECTOR('',#10532,2.);
#3041=VECTOR('',#10535,2.);
#3042=VECTOR('',#10538,2.);
#3043=VECTOR('',#10541,2.);
#3044=VECTOR('',#10544,1.5555);
#3045=VECTOR('',#10549,1.5555);
#3046=VECTOR('',#10552,1.5555);
#3047=VECTOR('',#10555,1.5555);
#3048=VECTOR('',#10558,1.5555);
#3049=VECTOR('',#10561,1.5555);
#3050=VECTOR('',#10564,1.5555);
#3051=VECTOR('',#10567,1.5555);
#3052=VECTOR('',#10570,1.5555);
#3053=VECTOR('',#10573,1.5555);
#3054=VECTOR('',#10578,1.5);
#3055=VECTOR('',#10589,10.);
#3056=VECTOR('',#10590,10.);
#3057=VECTOR('',#10591,10.);
#3058=VECTOR('',#10592,10.);
#3059=VECTOR('',#10595,10.);
#3060=VECTOR('',#10596,10.);
#3061=VECTOR('',#10597,10.);
#3062=VECTOR('',#10600,10.);
#3063=VECTOR('',#10601,10.);
#3064=VECTOR('',#10602,10.);
#3065=VECTOR('',#10605,10.);
#3066=VECTOR('',#10606,10.);
#3067=VECTOR('',#10607,10.);
#3068=VECTOR('',#10610,10.);
#3069=VECTOR('',#10611,10.);
#3070=VECTOR('',#10612,10.);
#3071=VECTOR('',#10615,10.);
#3072=VECTOR('',#10616,10.);
#3073=VECTOR('',#10625,3.5);
#3765=VERTEX_POINT('',#24324);
#3766=VERTEX_POINT('',#24325);
#3767=VERTEX_POINT('',#24327);
#3768=VERTEX_POINT('',#24338);
#3769=VERTEX_POINT('',#24348);
#3770=VERTEX_POINT('',#24349);
#3771=VERTEX_POINT('',#24396);
#3772=VERTEX_POINT('',#24397);
#3773=VERTEX_POINT('',#24444);
#3774=VERTEX_POINT('',#24445);
#3775=VERTEX_POINT('',#24495);
#3776=VERTEX_POINT('',#24496);
#3777=VERTEX_POINT('',#24546);
#3778=VERTEX_POINT('',#24547);
#3779=VERTEX_POINT('',#24594);
#3780=VERTEX_POINT('',#24595);
#3781=VERTEX_POINT('',#24642);
#3782=VERTEX_POINT('',#24643);
#3783=VERTEX_POINT('',#24696);
#3784=VERTEX_POINT('',#24697);
#3785=VERTEX_POINT('',#24744);
#3786=VERTEX_POINT('',#24745);
#3787=VERTEX_POINT('',#24792);
#3788=VERTEX_POINT('',#24793);
#3789=VERTEX_POINT('',#24795);
#3790=VERTEX_POINT('',#24806);
#3791=VERTEX_POINT('',#24817);
#3792=VERTEX_POINT('',#24818);
#3793=VERTEX_POINT('',#24842);
#3794=VERTEX_POINT('',#24843);
#3795=VERTEX_POINT('',#24866);
#3796=VERTEX_POINT('',#24867);
#3797=VERTEX_POINT('',#24891);
#3798=VERTEX_POINT('',#24892);
#3799=VERTEX_POINT('',#24916);
#3800=VERTEX_POINT('',#24917);
#3801=VERTEX_POINT('',#24940);
#3802=VERTEX_POINT('',#24941);
#3803=VERTEX_POINT('',#24964);
#3804=VERTEX_POINT('',#24965);
#3805=VERTEX_POINT('',#24990);
#3806=VERTEX_POINT('',#24991);
#3807=VERTEX_POINT('',#25014);
#3808=VERTEX_POINT('',#25015);
#3809=VERTEX_POINT('',#25038);
#3810=VERTEX_POINT('',#25244);
#3811=VERTEX_POINT('',#25303);
#3812=VERTEX_POINT('',#25333);
#3813=VERTEX_POINT('',#25616);
#3814=VERTEX_POINT('',#25730);
#3815=VERTEX_POINT('',#26135);
#3816=VERTEX_POINT('',#26136);
#3817=VERTEX_POINT('',#26138);
#3818=VERTEX_POINT('',#26140);
#3819=VERTEX_POINT('',#26144);
#3820=VERTEX_POINT('',#26146);
#3821=VERTEX_POINT('',#26150);
#3822=VERTEX_POINT('',#26152);
#3823=VERTEX_POINT('',#26156);
#3824=VERTEX_POINT('',#26158);
#3825=VERTEX_POINT('',#26162);
#3826=VERTEX_POINT('',#26164);
#3827=VERTEX_POINT('',#26172);
#3828=VERTEX_POINT('',#26175);
#4854=EDGE_CURVE('',#3765,#3766,#2488,.T.);
#4855=EDGE_CURVE('',#3765,#3767,#1960,.T.);
#4856=EDGE_CURVE('',#3767,#3768,#1520,.F.);
#4857=EDGE_CURVE('',#3768,#3766,#1961,.T.);
#4858=EDGE_CURVE('',#3769,#3770,#2489,.T.);
#4859=EDGE_CURVE('',#3769,#3765,#1962,.T.);
#4860=EDGE_CURVE('',#3766,#3770,#1963,.T.);
#4861=EDGE_CURVE('',#3771,#3772,#2490,.T.);
#4862=EDGE_CURVE('',#3771,#3769,#1964,.T.);
#4863=EDGE_CURVE('',#3770,#3772,#1965,.T.);
#4864=EDGE_CURVE('',#3773,#3774,#2491,.T.);
#4865=EDGE_CURVE('',#3773,#3771,#1966,.T.);
#4866=EDGE_CURVE('',#3772,#3774,#1967,.T.);
#4867=EDGE_CURVE('',#3775,#3776,#2492,.T.);
#4868=EDGE_CURVE('',#3775,#3773,#1968,.T.);
#4869=EDGE_CURVE('',#3774,#3776,#1969,.T.);
#4870=EDGE_CURVE('',#3777,#3778,#2493,.T.);
#4871=EDGE_CURVE('',#3777,#3775,#1970,.T.);
#4872=EDGE_CURVE('',#3776,#3778,#1971,.T.);
#4873=EDGE_CURVE('',#3779,#3780,#2494,.T.);
#4874=EDGE_CURVE('',#3779,#3777,#1972,.T.);
#4875=EDGE_CURVE('',#3778,#3780,#1973,.T.);
#4876=EDGE_CURVE('',#3781,#3782,#2495,.T.);
#4877=EDGE_CURVE('',#3781,#3779,#1974,.T.);
#4878=EDGE_CURVE('',#3780,#3782,#1975,.T.);
#4879=EDGE_CURVE('',#3783,#3784,#2496,.T.);
#4880=EDGE_CURVE('',#3783,#3781,#1976,.T.);
#4881=EDGE_CURVE('',#3782,#3784,#1977,.T.);
#4882=EDGE_CURVE('',#3785,#3786,#2497,.T.);
#4883=EDGE_CURVE('',#3785,#3783,#1978,.T.);
#4884=EDGE_CURVE('',#3784,#3786,#1979,.T.);
#4885=EDGE_CURVE('',#3787,#3788,#2498,.T.);
#4886=EDGE_CURVE('',#3787,#3789,#1980,.T.);
#4887=EDGE_CURVE('',#3789,#3790,#1521,.T.);
#4888=EDGE_CURVE('',#3788,#3790,#1981,.T.);
#4889=EDGE_CURVE('',#3791,#3792,#2499,.T.);
#4890=EDGE_CURVE('',#3791,#3787,#1982,.T.);
#4891=EDGE_CURVE('',#3792,#3788,#1983,.T.);
#4892=EDGE_CURVE('',#3793,#3794,#2500,.T.);
#4893=EDGE_CURVE('',#3793,#3791,#1984,.T.);
#4894=EDGE_CURVE('',#3794,#3792,#1985,.T.);
#4895=EDGE_CURVE('',#3795,#3796,#2501,.T.);
#4896=EDGE_CURVE('',#3795,#3793,#1986,.T.);
#4897=EDGE_CURVE('',#3796,#3794,#1987,.T.);
#4898=EDGE_CURVE('',#3797,#3798,#2502,.T.);
#4899=EDGE_CURVE('',#3797,#3795,#1988,.T.);
#4900=EDGE_CURVE('',#3798,#3796,#1989,.T.);
#4901=EDGE_CURVE('',#3799,#3800,#2503,.T.);
#4902=EDGE_CURVE('',#3799,#3797,#1990,.T.);
#4903=EDGE_CURVE('',#3800,#3798,#1991,.T.);
#4904=EDGE_CURVE('',#3801,#3802,#2504,.T.);
#4905=EDGE_CURVE('',#3801,#3799,#1992,.T.);
#4906=EDGE_CURVE('',#3802,#3800,#1993,.T.);
#4907=EDGE_CURVE('',#3803,#3804,#2505,.T.);
#4908=EDGE_CURVE('',#3803,#3801,#1994,.T.);
#4909=EDGE_CURVE('',#3804,#3802,#1995,.T.);
#4910=EDGE_CURVE('',#3805,#3806,#2506,.T.);
#4911=EDGE_CURVE('',#3805,#3803,#1996,.T.);
#4912=EDGE_CURVE('',#3806,#3804,#1997,.T.);
#4913=EDGE_CURVE('',#3807,#3808,#2507,.T.);
#4914=EDGE_CURVE('',#3807,#3805,#1998,.T.);
#4915=EDGE_CURVE('',#3808,#3806,#1999,.T.);
#4916=EDGE_CURVE('',#3790,#3809,#2000,.T.);
#4917=EDGE_CURVE('',#3810,#3789,#2001,.T.);
#4918=EDGE_CURVE('',#3811,#3810,#1522,.T.);
#4919=EDGE_CURVE('',#3809,#3811,#2002,.T.);
#4920=EDGE_CURVE('',#3809,#3812,#2508,.T.);
#4921=EDGE_CURVE('',#3812,#3812,#1523,.T.);
#4922=EDGE_CURVE('',#3813,#3807,#2003,.T.);
#4923=EDGE_CURVE('',#3767,#3813,#2004,.T.);
#4924=EDGE_CURVE('',#3810,#3785,#2005,.T.);
#4925=EDGE_CURVE('',#3814,#3808,#2006,.T.);
#4926=EDGE_CURVE('',#3813,#3814,#1524,.T.);
#4927=EDGE_CURVE('',#3786,#3811,#2007,.T.);
#4928=EDGE_CURVE('',#3814,#3768,#2008,.T.);
#4929=EDGE_CURVE('',#3815,#3816,#2509,.T.);
#4930=EDGE_CURVE('',#3815,#3817,#2510,.T.);
#4931=EDGE_CURVE('',#3817,#3818,#2511,.T.);
#4932=EDGE_CURVE('',#3816,#3818,#2512,.T.);
#4933=EDGE_CURVE('',#3819,#3815,#2513,.T.);
#4934=EDGE_CURVE('',#3819,#3820,#2514,.T.);
#4935=EDGE_CURVE('',#3820,#3817,#2515,.T.);
#4936=EDGE_CURVE('',#3821,#3819,#2516,.T.);
#4937=EDGE_CURVE('',#3821,#3822,#2517,.T.);
#4938=EDGE_CURVE('',#3822,#3820,#2518,.T.);
#4939=EDGE_CURVE('',#3823,#3821,#2519,.T.);
#4940=EDGE_CURVE('',#3823,#3824,#2520,.T.);
#4941=EDGE_CURVE('',#3824,#3822,#2521,.T.);
#4942=EDGE_CURVE('',#3825,#3823,#2522,.T.);
#4943=EDGE_CURVE('',#3825,#3826,#2523,.T.);
#4944=EDGE_CURVE('',#3826,#3824,#2524,.T.);
#4945=EDGE_CURVE('',#3816,#3825,#2525,.T.);
#4946=EDGE_CURVE('',#3818,#3826,#2526,.T.);
#4947=EDGE_CURVE('',#3827,#3827,#1525,.T.);
#4948=EDGE_CURVE('',#3827,#3828,#2527,.T.);
#4949=EDGE_CURVE('',#3828,#3828,#1526,.T.);
#6861=ORIENTED_EDGE('',*,*,#4854,.F.);
#6862=ORIENTED_EDGE('',*,*,#4855,.T.);
#6863=ORIENTED_EDGE('',*,*,#4856,.T.);
#6864=ORIENTED_EDGE('',*,*,#4857,.T.);
#6865=ORIENTED_EDGE('',*,*,#4858,.F.);
#6866=ORIENTED_EDGE('',*,*,#4859,.T.);
#6867=ORIENTED_EDGE('',*,*,#4854,.T.);
#6868=ORIENTED_EDGE('',*,*,#4860,.T.);
#6869=ORIENTED_EDGE('',*,*,#4861,.F.);
#6870=ORIENTED_EDGE('',*,*,#4862,.T.);
#6871=ORIENTED_EDGE('',*,*,#4858,.T.);
#6872=ORIENTED_EDGE('',*,*,#4863,.T.);
#6873=ORIENTED_EDGE('',*,*,#4864,.F.);
#6874=ORIENTED_EDGE('',*,*,#4865,.T.);
#6875=ORIENTED_EDGE('',*,*,#4861,.T.);
#6876=ORIENTED_EDGE('',*,*,#4866,.T.);
#6877=ORIENTED_EDGE('',*,*,#4867,.F.);
#6878=ORIENTED_EDGE('',*,*,#4868,.T.);
#6879=ORIENTED_EDGE('',*,*,#4864,.T.);
#6880=ORIENTED_EDGE('',*,*,#4869,.T.);
#6881=ORIENTED_EDGE('',*,*,#4870,.F.);
#6882=ORIENTED_EDGE('',*,*,#4871,.T.);
#6883=ORIENTED_EDGE('',*,*,#4867,.T.);
#6884=ORIENTED_EDGE('',*,*,#4872,.T.);
#6885=ORIENTED_EDGE('',*,*,#4873,.F.);
#6886=ORIENTED_EDGE('',*,*,#4874,.T.);
#6887=ORIENTED_EDGE('',*,*,#4870,.T.);
#6888=ORIENTED_EDGE('',*,*,#4875,.T.);
#6889=ORIENTED_EDGE('',*,*,#4876,.F.);
#6890=ORIENTED_EDGE('',*,*,#4877,.T.);
#6891=ORIENTED_EDGE('',*,*,#4873,.T.);
#6892=ORIENTED_EDGE('',*,*,#4878,.T.);
#6893=ORIENTED_EDGE('',*,*,#4879,.F.);
#6894=ORIENTED_EDGE('',*,*,#4880,.T.);
#6895=ORIENTED_EDGE('',*,*,#4876,.T.);
#6896=ORIENTED_EDGE('',*,*,#4881,.T.);
#6897=ORIENTED_EDGE('',*,*,#4882,.F.);
#6898=ORIENTED_EDGE('',*,*,#4883,.T.);
#6899=ORIENTED_EDGE('',*,*,#4879,.T.);
#6900=ORIENTED_EDGE('',*,*,#4884,.T.);
#6901=ORIENTED_EDGE('',*,*,#4885,.F.);
#6902=ORIENTED_EDGE('',*,*,#4886,.T.);
#6903=ORIENTED_EDGE('',*,*,#4887,.T.);
#6904=ORIENTED_EDGE('',*,*,#4888,.F.);
#6905=ORIENTED_EDGE('',*,*,#4889,.F.);
#6906=ORIENTED_EDGE('',*,*,#4890,.T.);
#6907=ORIENTED_EDGE('',*,*,#4885,.T.);
#6908=ORIENTED_EDGE('',*,*,#4891,.F.);
#6909=ORIENTED_EDGE('',*,*,#4892,.F.);
#6910=ORIENTED_EDGE('',*,*,#4893,.T.);
#6911=ORIENTED_EDGE('',*,*,#4889,.T.);
#6912=ORIENTED_EDGE('',*,*,#4894,.F.);
#6913=ORIENTED_EDGE('',*,*,#4895,.F.);
#6914=ORIENTED_EDGE('',*,*,#4896,.T.);
#6915=ORIENTED_EDGE('',*,*,#4892,.T.);
#6916=ORIENTED_EDGE('',*,*,#4897,.F.);
#6917=ORIENTED_EDGE('',*,*,#4898,.F.);
#6918=ORIENTED_EDGE('',*,*,#4899,.T.);
#6919=ORIENTED_EDGE('',*,*,#4895,.T.);
#6920=ORIENTED_EDGE('',*,*,#4900,.F.);
#6921=ORIENTED_EDGE('',*,*,#4901,.F.);
#6922=ORIENTED_EDGE('',*,*,#4902,.T.);
#6923=ORIENTED_EDGE('',*,*,#4898,.T.);
#6924=ORIENTED_EDGE('',*,*,#4903,.F.);
#6925=ORIENTED_EDGE('',*,*,#4904,.F.);
#6926=ORIENTED_EDGE('',*,*,#4905,.T.);
#6927=ORIENTED_EDGE('',*,*,#4901,.T.);
#6928=ORIENTED_EDGE('',*,*,#4906,.F.);
#6929=ORIENTED_EDGE('',*,*,#4907,.F.);
#6930=ORIENTED_EDGE('',*,*,#4908,.T.);
#6931=ORIENTED_EDGE('',*,*,#4904,.T.);
#6932=ORIENTED_EDGE('',*,*,#4909,.F.);
#6933=ORIENTED_EDGE('',*,*,#4910,.F.);
#6934=ORIENTED_EDGE('',*,*,#4911,.T.);
#6935=ORIENTED_EDGE('',*,*,#4907,.T.);
#6936=ORIENTED_EDGE('',*,*,#4912,.F.);
#6937=ORIENTED_EDGE('',*,*,#4913,.F.);
#6938=ORIENTED_EDGE('',*,*,#4914,.T.);
#6939=ORIENTED_EDGE('',*,*,#4910,.T.);
#6940=ORIENTED_EDGE('',*,*,#4915,.F.);
#6941=ORIENTED_EDGE('',*,*,#4916,.F.);
#6942=ORIENTED_EDGE('',*,*,#4887,.F.);
#6943=ORIENTED_EDGE('',*,*,#4917,.F.);
#6944=ORIENTED_EDGE('',*,*,#4918,.F.);
#6945=ORIENTED_EDGE('',*,*,#4919,.F.);
#6946=ORIENTED_EDGE('',*,*,#4920,.T.);
#6947=ORIENTED_EDGE('',*,*,#4921,.F.);
#6948=ORIENTED_EDGE('',*,*,#4920,.F.);
#6949=ORIENTED_EDGE('',*,*,#4917,.T.);
#6950=ORIENTED_EDGE('',*,*,#4886,.F.);
#6951=ORIENTED_EDGE('',*,*,#4890,.F.);
#6952=ORIENTED_EDGE('',*,*,#4893,.F.);
#6953=ORIENTED_EDGE('',*,*,#4896,.F.);
#6954=ORIENTED_EDGE('',*,*,#4899,.F.);
#6955=ORIENTED_EDGE('',*,*,#4902,.F.);
#6956=ORIENTED_EDGE('',*,*,#4905,.F.);
#6957=ORIENTED_EDGE('',*,*,#4908,.F.);
#6958=ORIENTED_EDGE('',*,*,#4911,.F.);
#6959=ORIENTED_EDGE('',*,*,#4914,.F.);
#6960=ORIENTED_EDGE('',*,*,#4922,.F.);
#6961=ORIENTED_EDGE('',*,*,#4923,.F.);
#6962=ORIENTED_EDGE('',*,*,#4855,.F.);
#6963=ORIENTED_EDGE('',*,*,#4859,.F.);
#6964=ORIENTED_EDGE('',*,*,#4862,.F.);
#6965=ORIENTED_EDGE('',*,*,#4865,.F.);
#6966=ORIENTED_EDGE('',*,*,#4868,.F.);
#6967=ORIENTED_EDGE('',*,*,#4871,.F.);
#6968=ORIENTED_EDGE('',*,*,#4874,.F.);
#6969=ORIENTED_EDGE('',*,*,#4877,.F.);
#6970=ORIENTED_EDGE('',*,*,#4880,.F.);
#6971=ORIENTED_EDGE('',*,*,#4883,.F.);
#6972=ORIENTED_EDGE('',*,*,#4924,.F.);
#6973=ORIENTED_EDGE('',*,*,#4913,.T.);
#6974=ORIENTED_EDGE('',*,*,#4925,.F.);
#6975=ORIENTED_EDGE('',*,*,#4926,.F.);
#6976=ORIENTED_EDGE('',*,*,#4922,.T.);
#6977=ORIENTED_EDGE('',*,*,#4916,.T.);
#6978=ORIENTED_EDGE('',*,*,#4919,.T.);
#6979=ORIENTED_EDGE('',*,*,#4927,.F.);
#6980=ORIENTED_EDGE('',*,*,#4884,.F.);
#6981=ORIENTED_EDGE('',*,*,#4881,.F.);
#6982=ORIENTED_EDGE('',*,*,#4878,.F.);
#6983=ORIENTED_EDGE('',*,*,#4875,.F.);
#6984=ORIENTED_EDGE('',*,*,#4872,.F.);
#6985=ORIENTED_EDGE('',*,*,#4869,.F.);
#6986=ORIENTED_EDGE('',*,*,#4866,.F.);
#6987=ORIENTED_EDGE('',*,*,#4863,.F.);
#6988=ORIENTED_EDGE('',*,*,#4860,.F.);
#6989=ORIENTED_EDGE('',*,*,#4857,.F.);
#6990=ORIENTED_EDGE('',*,*,#4928,.F.);
#6991=ORIENTED_EDGE('',*,*,#4925,.T.);
#6992=ORIENTED_EDGE('',*,*,#4915,.T.);
#6993=ORIENTED_EDGE('',*,*,#4912,.T.);
#6994=ORIENTED_EDGE('',*,*,#4909,.T.);
#6995=ORIENTED_EDGE('',*,*,#4906,.T.);
#6996=ORIENTED_EDGE('',*,*,#4903,.T.);
#6997=ORIENTED_EDGE('',*,*,#4900,.T.);
#6998=ORIENTED_EDGE('',*,*,#4897,.T.);
#6999=ORIENTED_EDGE('',*,*,#4894,.T.);
#7000=ORIENTED_EDGE('',*,*,#4891,.T.);
#7001=ORIENTED_EDGE('',*,*,#4888,.T.);
#7002=ORIENTED_EDGE('',*,*,#4882,.T.);
#7003=ORIENTED_EDGE('',*,*,#4927,.T.);
#7004=ORIENTED_EDGE('',*,*,#4918,.T.);
#7005=ORIENTED_EDGE('',*,*,#4924,.T.);
#7006=ORIENTED_EDGE('',*,*,#4929,.F.);
#7007=ORIENTED_EDGE('',*,*,#4930,.T.);
#7008=ORIENTED_EDGE('',*,*,#4931,.T.);
#7009=ORIENTED_EDGE('',*,*,#4932,.F.);
#7010=ORIENTED_EDGE('',*,*,#4933,.F.);
#7011=ORIENTED_EDGE('',*,*,#4934,.T.);
#7012=ORIENTED_EDGE('',*,*,#4935,.T.);
#7013=ORIENTED_EDGE('',*,*,#4930,.F.);
#7014=ORIENTED_EDGE('',*,*,#4936,.F.);
#7015=ORIENTED_EDGE('',*,*,#4937,.T.);
#7016=ORIENTED_EDGE('',*,*,#4938,.T.);
#7017=ORIENTED_EDGE('',*,*,#4934,.F.);
#7018=ORIENTED_EDGE('',*,*,#4939,.F.);
#7019=ORIENTED_EDGE('',*,*,#4940,.T.);
#7020=ORIENTED_EDGE('',*,*,#4941,.T.);
#7021=ORIENTED_EDGE('',*,*,#4937,.F.);
#7022=ORIENTED_EDGE('',*,*,#4942,.F.);
#7023=ORIENTED_EDGE('',*,*,#4943,.T.);
#7024=ORIENTED_EDGE('',*,*,#4944,.T.);
#7025=ORIENTED_EDGE('',*,*,#4940,.F.);
#7026=ORIENTED_EDGE('',*,*,#4945,.F.);
#7027=ORIENTED_EDGE('',*,*,#4932,.T.);
#7028=ORIENTED_EDGE('',*,*,#4946,.T.);
#7029=ORIENTED_EDGE('',*,*,#4943,.F.);
#7030=ORIENTED_EDGE('',*,*,#4946,.F.);
#7031=ORIENTED_EDGE('',*,*,#4931,.F.);
#7032=ORIENTED_EDGE('',*,*,#4935,.F.);
#7033=ORIENTED_EDGE('',*,*,#4938,.F.);
#7034=ORIENTED_EDGE('',*,*,#4941,.F.);
#7035=ORIENTED_EDGE('',*,*,#4944,.F.);
#7036=ORIENTED_EDGE('',*,*,#4947,.T.);
#7037=ORIENTED_EDGE('',*,*,#4923,.T.);
#7038=ORIENTED_EDGE('',*,*,#4926,.T.);
#7039=ORIENTED_EDGE('',*,*,#4928,.T.);
#7040=ORIENTED_EDGE('',*,*,#4856,.F.);
#7041=ORIENTED_EDGE('',*,*,#4947,.F.);
#7042=ORIENTED_EDGE('',*,*,#4948,.T.);
#7043=ORIENTED_EDGE('',*,*,#4949,.T.);
#7044=ORIENTED_EDGE('',*,*,#4948,.F.);
#7045=ORIENTED_EDGE('',*,*,#4949,.F.);
#7046=ORIENTED_EDGE('',*,*,#4929,.T.);
#7047=ORIENTED_EDGE('',*,*,#4945,.T.);
#7048=ORIENTED_EDGE('',*,*,#4942,.T.);
#7049=ORIENTED_EDGE('',*,*,#4939,.T.);
#7050=ORIENTED_EDGE('',*,*,#4936,.T.);
#7051=ORIENTED_EDGE('',*,*,#4933,.T.);
#7052=ORIENTED_EDGE('',*,*,#4921,.T.);
#8079=CYLINDRICAL_SURFACE('',#9226,1.954);
#8080=CYLINDRICAL_SURFACE('',#9228,1.954);
#8081=CYLINDRICAL_SURFACE('',#9229,1.954);
#8082=CYLINDRICAL_SURFACE('',#9230,1.954);
#8083=CYLINDRICAL_SURFACE('',#9231,1.954);
#8084=CYLINDRICAL_SURFACE('',#9232,1.954);
#8085=CYLINDRICAL_SURFACE('',#9233,1.954);
#8086=CYLINDRICAL_SURFACE('',#9234,1.954);
#8087=CYLINDRICAL_SURFACE('',#9235,1.954);
#8088=CYLINDRICAL_SURFACE('',#9236,1.954);
#8089=CYLINDRICAL_SURFACE('',#9237,1.5555);
#8090=CYLINDRICAL_SURFACE('',#9239,1.5555);
#8091=CYLINDRICAL_SURFACE('',#9240,1.5555);
#8092=CYLINDRICAL_SURFACE('',#9241,1.5555);
#8093=CYLINDRICAL_SURFACE('',#9242,1.5555);
#8094=CYLINDRICAL_SURFACE('',#9243,1.5555);
#8095=CYLINDRICAL_SURFACE('',#9244,1.5555);
#8096=CYLINDRICAL_SURFACE('',#9245,1.5555);
#8097=CYLINDRICAL_SURFACE('',#9246,1.5555);
#8098=CYLINDRICAL_SURFACE('',#9247,1.5555);
#8099=CYLINDRICAL_SURFACE('',#9251,1.5555);
#8100=CYLINDRICAL_SURFACE('',#9253,1.954);
#8101=CYLINDRICAL_SURFACE('',#9263,3.5);
#8475=ADVANCED_FACE('',(#727),#8079,.T.);
#8476=ADVANCED_FACE('',(#728),#8080,.T.);
#8477=ADVANCED_FACE('',(#729),#8081,.T.);
#8478=ADVANCED_FACE('',(#730),#8082,.T.);
#8479=ADVANCED_FACE('',(#731),#8083,.T.);
#8480=ADVANCED_FACE('',(#732),#8084,.T.);
#8481=ADVANCED_FACE('',(#733),#8085,.T.);
#8482=ADVANCED_FACE('',(#734),#8086,.T.);
#8483=ADVANCED_FACE('',(#735),#8087,.T.);
#8484=ADVANCED_FACE('',(#736),#8088,.T.);
#8485=ADVANCED_FACE('',(#737),#8089,.T.);
#8486=ADVANCED_FACE('',(#738),#8090,.T.);
#8487=ADVANCED_FACE('',(#739),#8091,.T.);
#8488=ADVANCED_FACE('',(#740),#8092,.T.);
#8489=ADVANCED_FACE('',(#741),#8093,.T.);
#8490=ADVANCED_FACE('',(#742),#8094,.T.);
#8491=ADVANCED_FACE('',(#743),#8095,.T.);
#8492=ADVANCED_FACE('',(#744),#8096,.T.);
#8493=ADVANCED_FACE('',(#745),#8097,.T.);
#8494=ADVANCED_FACE('',(#746),#8098,.T.);
#8495=ADVANCED_FACE('',(#747),#159,.T.);
#8496=ADVANCED_FACE('',(#748),#303,.F.);
#8497=ADVANCED_FACE('',(#749),#8099,.T.);
#8498=ADVANCED_FACE('',(#750),#304,.F.);
#8499=ADVANCED_FACE('',(#751),#8100,.T.);
#8500=ADVANCED_FACE('',(#752),#384,.F.);
#8501=ADVANCED_FACE('',(#753),#385,.F.);
#8502=ADVANCED_FACE('',(#754),#386,.F.);
#8503=ADVANCED_FACE('',(#755),#387,.F.);
#8504=ADVANCED_FACE('',(#756),#388,.F.);
#8505=ADVANCED_FACE('',(#757),#389,.F.);
#8506=ADVANCED_FACE('',(#758),#390,.F.);
#8507=ADVANCED_FACE('',(#759,#264),#391,.T.);
#8508=ADVANCED_FACE('',(#760),#8101,.T.);
#8509=ADVANCED_FACE('',(#761,#265),#392,.F.);
#8510=ADVANCED_FACE('',(#762),#393,.T.);
#8683=CLOSED_SHELL('',(#8475,#8476,#8477,#8478,#8479,#8480,#8481,#8482,
#8483,#8484,#8485,#8486,#8487,#8488,#8489,#8490,#8491,#8492,#8493,#8494,
#8495,#8496,#8497,#8498,#8499,#8500,#8501,#8502,#8503,#8504,#8505,#8506,
#8507,#8508,#8509,#8510));
#9225=AXIS2_PLACEMENT_3D('',#24322,#10508,#10509);
#9226=AXIS2_PLACEMENT_3D('',#24323,#10510,#10511);
#9227=AXIS2_PLACEMENT_3D('',#24339,#10513,#10514);
#9228=AXIS2_PLACEMENT_3D('',#24347,#10515,#10516);
#9229=AXIS2_PLACEMENT_3D('',#24395,#10518,#10519);
#9230=AXIS2_PLACEMENT_3D('',#24443,#10521,#10522);
#9231=AXIS2_PLACEMENT_3D('',#24494,#10524,#10525);
#9232=AXIS2_PLACEMENT_3D('',#24545,#10527,#10528);
#9233=AXIS2_PLACEMENT_3D('',#24593,#10530,#10531);
#9234=AXIS2_PLACEMENT_3D('',#24641,#10533,#10534);
#9235=AXIS2_PLACEMENT_3D('',#24695,#10536,#10537);
#9236=AXIS2_PLACEMENT_3D('',#24743,#10539,#10540);
#9237=AXIS2_PLACEMENT_3D('',#24791,#10542,#10543);
#9238=AXIS2_PLACEMENT_3D('',#24807,#10545,#10546);
#9239=AXIS2_PLACEMENT_3D('',#24816,#10547,#10548);
#9240=AXIS2_PLACEMENT_3D('',#24841,#10550,#10551);
#9241=AXIS2_PLACEMENT_3D('',#24865,#10553,#10554);
#9242=AXIS2_PLACEMENT_3D('',#24890,#10556,#10557);
#9243=AXIS2_PLACEMENT_3D('',#24915,#10559,#10560);
#9244=AXIS2_PLACEMENT_3D('',#24939,#10562,#10563);
#9245=AXIS2_PLACEMENT_3D('',#24963,#10565,#10566);
#9246=AXIS2_PLACEMENT_3D('',#24989,#10568,#10569);
#9247=AXIS2_PLACEMENT_3D('',#25013,#10571,#10572);
#9248=AXIS2_PLACEMENT_3D('',#25037,#10574,#10575);
#9249=AXIS2_PLACEMENT_3D('',#25304,#10576,#10577);
#9250=AXIS2_PLACEMENT_3D('',#25335,#10579,#10580);
#9251=AXIS2_PLACEMENT_3D('',#25729,#10581,#10582);
#9252=AXIS2_PLACEMENT_3D('',#25740,#10583,#10584);
#9253=AXIS2_PLACEMENT_3D('',#26133,#10585,#10586);
#9254=AXIS2_PLACEMENT_3D('',#26134,#10587,#10588);
#9255=AXIS2_PLACEMENT_3D('',#26143,#10593,#10594);
#9256=AXIS2_PLACEMENT_3D('',#26149,#10598,#10599);
#9257=AXIS2_PLACEMENT_3D('',#26155,#10603,#10604);
#9258=AXIS2_PLACEMENT_3D('',#26161,#10608,#10609);
#9259=AXIS2_PLACEMENT_3D('',#26167,#10613,#10614);
#9260=AXIS2_PLACEMENT_3D('',#26170,#10617,#10618);
#9261=AXIS2_PLACEMENT_3D('',#26171,#10619,#10620);
#9262=AXIS2_PLACEMENT_3D('',#26173,#10621,#10622);
#9263=AXIS2_PLACEMENT_3D('',#26174,#10623,#10624);
#9264=AXIS2_PLACEMENT_3D('',#26177,#10626,#10627);
#9265=AXIS2_PLACEMENT_3D('',#26178,#10628,#10629);
#9266=AXIS2_PLACEMENT_3D('',#26179,#10630,#10631);
#10508=DIRECTION('axis',(0.,0.,1.));
#10509=DIRECTION('refdir',(1.,0.,0.));
#10510=DIRECTION('center_axis',(0.,0.,1.));
#10511=DIRECTION('ref_axis',(1.,0.,0.));
#10512=DIRECTION('',(0.,0.,-1.));
#10513=DIRECTION('center_axis',(0.,0.,-1.));
#10514=DIRECTION('ref_axis',(1.,0.,0.));
#10515=DIRECTION('center_axis',(0.,0.,1.));
#10516=DIRECTION('ref_axis',(1.,0.,0.));
#10517=DIRECTION('',(0.,0.,-1.));
#10518=DIRECTION('center_axis',(0.,0.,1.));
#10519=DIRECTION('ref_axis',(1.,0.,0.));
#10520=DIRECTION('',(0.,0.,-1.));
#10521=DIRECTION('center_axis',(0.,0.,1.));
#10522=DIRECTION('ref_axis',(1.,0.,0.));
#10523=DIRECTION('',(0.,0.,-1.));
#10524=DIRECTION('center_axis',(0.,0.,1.));
#10525=DIRECTION('ref_axis',(1.,0.,0.));
#10526=DIRECTION('',(0.,0.,-1.));
#10527=DIRECTION('center_axis',(0.,0.,1.));
#10528=DIRECTION('ref_axis',(1.,0.,0.));
#10529=DIRECTION('',(0.,0.,-1.));
#10530=DIRECTION('center_axis',(0.,0.,1.));
#10531=DIRECTION('ref_axis',(1.,0.,0.));
#10532=DIRECTION('',(0.,0.,-1.));
#10533=DIRECTION('center_axis',(0.,0.,1.));
#10534=DIRECTION('ref_axis',(1.,0.,0.));
#10535=DIRECTION('',(0.,0.,-1.));
#10536=DIRECTION('center_axis',(0.,0.,1.));
#10537=DIRECTION('ref_axis',(1.,0.,0.));
#10538=DIRECTION('',(0.,0.,-1.));
#10539=DIRECTION('center_axis',(0.,0.,1.));
#10540=DIRECTION('ref_axis',(1.,0.,0.));
#10541=DIRECTION('',(0.,0.,-1.));
#10542=DIRECTION('center_axis',(0.,0.,1.));
#10543=DIRECTION('ref_axis',(0.99867308056793,-0.051498331516286,0.));
#10544=DIRECTION('',(0.,0.,1.));
#10545=DIRECTION('center_axis',(0.,0.,-1.));
#10546=DIRECTION('ref_axis',(1.,5.83250561478606E-14,0.));
#10547=DIRECTION('center_axis',(0.,0.,1.));
#10548=DIRECTION('ref_axis',(1.,5.83250561478606E-14,0.));
#10549=DIRECTION('',(0.,0.,1.));
#10550=DIRECTION('center_axis',(0.,0.,1.));
#10551=DIRECTION('ref_axis',(1.,5.83250561478606E-14,0.));
#10552=DIRECTION('',(0.,0.,1.));
#10553=DIRECTION('center_axis',(0.,0.,1.));
#10554=DIRECTION('ref_axis',(1.,5.83250561478606E-14,0.));
#10555=DIRECTION('',(0.,0.,1.));
#10556=DIRECTION('center_axis',(0.,0.,1.));
#10557=DIRECTION('ref_axis',(1.,5.83250561478606E-14,0.));
#10558=DIRECTION('',(0.,0.,1.));
#10559=DIRECTION('center_axis',(0.,0.,1.));
#10560=DIRECTION('ref_axis',(1.,5.83250561478606E-14,0.));
#10561=DIRECTION('',(0.,0.,1.));
#10562=DIRECTION('center_axis',(0.,0.,1.));
#10563=DIRECTION('ref_axis',(1.,5.83250561478606E-14,0.));
#10564=DIRECTION('',(0.,0.,1.));
#10565=DIRECTION('center_axis',(0.,0.,1.));
#10566=DIRECTION('ref_axis',(1.,5.83250561478606E-14,0.));
#10567=DIRECTION('',(0.,0.,1.));
#10568=DIRECTION('center_axis',(0.,0.,1.));
#10569=DIRECTION('ref_axis',(1.,5.83250561478606E-14,0.));
#10570=DIRECTION('',(0.,0.,1.));
#10571=DIRECTION('center_axis',(0.,0.,1.));
#10572=DIRECTION('ref_axis',(1.,5.83250561478606E-14,0.));
#10573=DIRECTION('',(0.,0.,1.));
#10574=DIRECTION('center_axis',(0.,0.,-1.));
#10575=DIRECTION('ref_axis',(1.,0.,0.));
#10576=DIRECTION('center_axis',(0.,0.,-1.));
#10577=DIRECTION('ref_axis',(1.,0.,0.));
#10578=DIRECTION('',(0.707106781186547,8.65956056235493E-17,0.707106781186548));
#10579=DIRECTION('center_axis',(0.,0.,1.));
#10580=DIRECTION('ref_axis',(1.,0.,0.));
#10581=DIRECTION('center_axis',(0.,0.,1.));
#10582=DIRECTION('ref_axis',(1.,5.83250561478606E-14,0.));
#10583=DIRECTION('center_axis',(0.,0.,-1.));
#10584=DIRECTION('ref_axis',(1.,5.83250561478606E-14,0.));
#10585=DIRECTION('center_axis',(0.,0.,1.));
#10586=DIRECTION('ref_axis',(1.,0.,0.));
#10587=DIRECTION('center_axis',(-1.60246890531964E-16,-1.,0.));
#10588=DIRECTION('ref_axis',(1.,-1.60246890531964E-16,0.));
#10589=DIRECTION('',(1.,-1.60246890531964E-16,0.));
#10590=DIRECTION('',(0.,0.,1.));
#10591=DIRECTION('',(1.,-1.60246890531964E-16,0.));
#10592=DIRECTION('',(0.,0.,1.));
#10593=DIRECTION('center_axis',(-0.866025403784439,-0.5,0.));
#10594=DIRECTION('ref_axis',(0.5,-0.866025403784439,0.));
#10595=DIRECTION('',(0.5,-0.866025403784439,0.));
#10596=DIRECTION('',(0.,0.,1.));
#10597=DIRECTION('',(0.5,-0.866025403784439,0.));
#10598=DIRECTION('center_axis',(-0.866025403784439,0.5,0.));
#10599=DIRECTION('ref_axis',(-0.5,-0.866025403784439,0.));
#10600=DIRECTION('',(-0.5,-0.866025403784439,0.));
#10601=DIRECTION('',(0.,0.,1.));
#10602=DIRECTION('',(-0.5,-0.866025403784439,0.));
#10603=DIRECTION('center_axis',(1.60246890531964E-16,1.,0.));
#10604=DIRECTION('ref_axis',(-1.,1.60246890531964E-16,0.));
#10605=DIRECTION('',(-1.,1.60246890531964E-16,0.));
#10606=DIRECTION('',(0.,0.,1.));
#10607=DIRECTION('',(-1.,1.60246890531964E-16,0.));
#10608=DIRECTION('center_axis',(0.866025403784439,0.5,0.));
#10609=DIRECTION('ref_axis',(-0.5,0.866025403784439,0.));
#10610=DIRECTION('',(-0.5,0.866025403784439,0.));
#10611=DIRECTION('',(0.,0.,1.));
#10612=DIRECTION('',(-0.5,0.866025403784439,0.));
#10613=DIRECTION('center_axis',(0.866025403784439,-0.5,0.));
#10614=DIRECTION('ref_axis',(0.5,0.866025403784439,0.));
#10615=DIRECTION('',(0.5,0.866025403784439,0.));
#10616=DIRECTION('',(0.5,0.866025403784439,0.));
#10617=DIRECTION('center_axis',(0.,0.,1.));
#10618=DIRECTION('ref_axis',(1.,0.,0.));
#10619=DIRECTION('center_axis',(0.,0.,1.));
#10620=DIRECTION('ref_axis',(1.,0.,0.));
#10621=DIRECTION('center_axis',(0.,0.,1.));
#10622=DIRECTION('ref_axis',(1.,0.,0.));
#10623=DIRECTION('center_axis',(0.,0.,1.));
#10624=DIRECTION('ref_axis',(1.,0.,0.));
#10625=DIRECTION('',(0.,0.,-1.));
#10626=DIRECTION('center_axis',(0.,0.,1.));
#10627=DIRECTION('ref_axis',(1.,0.,0.));
#10628=DIRECTION('center_axis',(0.,0.,1.));
#10629=DIRECTION('ref_axis',(1.,0.,0.));
#10630=DIRECTION('center_axis',(0.,0.,1.));
#10631=DIRECTION('ref_axis',(1.,0.,0.));
#24322=CARTESIAN_POINT('',(0.,0.,0.));
#24323=CARTESIAN_POINT('Origin',(0.,0.,0.));
#24324=CARTESIAN_POINT('',(-1.95633598837559,0.00127248296362327,0.22586969212423));
#24325=CARTESIAN_POINT('',(-1.95588590413641,0.00206796222160181,0.124130307875766));
#24326=CARTESIAN_POINT('',(-1.954,-2.39295984553393E-16,0.));
#24327=CARTESIAN_POINT('',(0.861525859670522,1.75382131162755,0.));
#24328=CARTESIAN_POINT('Ctrl Pts',(-1.95633598837559,0.00127248296362327,
0.22586969212423));
#24329=CARTESIAN_POINT('Ctrl Pts',(-1.95680065536751,0.06824838727295,0.222037687723474));
#24330=CARTESIAN_POINT('Ctrl Pts',(-1.95366001618977,0.135177367276064,
0.218205683322718));
#24331=CARTESIAN_POINT('Ctrl Pts',(-1.9467704464542,0.201714622162032,0.214373678921962));
#24332=CARTESIAN_POINT('Ctrl Pts',(-1.88018097341933,0.844814396182631,
0.177336365489126));
#24333=CARTESIAN_POINT('Ctrl Pts',(-1.46337681650964,1.45132029737704,0.140299052056291));
#24334=CARTESIAN_POINT('Ctrl Pts',(-0.886898775458456,1.74452597744752,
0.103261738623455));
#24335=CARTESIAN_POINT('Ctrl Pts',(-0.351149650411554,2.01701629862282,
0.0688411590823035));
#24336=CARTESIAN_POINT('Ctrl Pts',(0.32250805655704,2.01891265608728,0.0344205795411517));
#24337=CARTESIAN_POINT('Ctrl Pts',(0.863568564283469,1.75641400930303,6.50521303491303E-18));
#24338=CARTESIAN_POINT('',(-0.861525859670545,1.75382131162753,0.));
#24339=CARTESIAN_POINT('Origin',(0.,0.,0.));
#24340=CARTESIAN_POINT('Ctrl Pts',(-0.861525859670546,1.75382131162753,
1.07552855510562E-15));
#24341=CARTESIAN_POINT('Ctrl Pts',(-1.44517400349648,1.46711709294739,0.0370752371124262));
#24342=CARTESIAN_POINT('Ctrl Pts',(-1.86938639577653,0.868642989156275,
0.0741504742248514));
#24343=CARTESIAN_POINT('Ctrl Pts',(-1.94388330047271,0.2267475072264,0.111225711337276));
#24344=CARTESIAN_POINT('Ctrl Pts',(-1.95252655828524,0.15227369973538,0.115527243516773));
#24345=CARTESIAN_POINT('Ctrl Pts',(-1.95646228341413,0.0772153955205521,
0.119828775696269));
#24346=CARTESIAN_POINT('Ctrl Pts',(-1.95588590413641,0.00206796222160181,
0.124130307875766));
#24347=CARTESIAN_POINT('Origin',(0.,0.,0.));
#24348=CARTESIAN_POINT('',(-1.95128265771456,0.000979968443958618,0.92586969212423));
#24349=CARTESIAN_POINT('',(-1.95120671878141,0.0009421225145049,0.824130307875766));
#24350=CARTESIAN_POINT('',(-1.954,-2.39295984553393E-16,0.));
#24351=CARTESIAN_POINT('Ctrl Pts',(-1.95128265771456,0.000979968443958618,
0.92586969212423));
#24352=CARTESIAN_POINT('Ctrl Pts',(-1.95247392016078,0.26388492489574,0.910928234987155));
#24353=CARTESIAN_POINT('Ctrl Pts',(-1.90305890226364,0.526360198569273,
0.895986777850081));
#24354=CARTESIAN_POINT('Ctrl Pts',(-1.80091082202569,0.76639335768976,0.881045320713007));
#24355=CARTESIAN_POINT('Ctrl Pts',(-1.54770322455863,1.36139445209842,0.844008007280172));
#24356=CARTESIAN_POINT('Ctrl Pts',(-0.970472477077253,1.8184979102298,0.806970693847336));
#24357=CARTESIAN_POINT('Ctrl Pts',(-0.333275819998743,1.92861264524847,
0.7699333804145));
#24358=CARTESIAN_POINT('Ctrl Pts',(0.303920837079767,2.03872738026714,0.732896066981664));
#24359=CARTESIAN_POINT('Ctrl Pts',(1.00108340375541,1.8018533921731,0.695858753548828));
#24360=CARTESIAN_POINT('Ctrl Pts',(1.43928269883041,1.32632160988724,0.658821440115992));
#24361=CARTESIAN_POINT('Ctrl Pts',(1.87748199390539,0.850789827601394,0.621784126683156));
#24362=CARTESIAN_POINT('Ctrl Pts',(2.05671801737973,0.13660025112374,0.584746813250321));
#24363=CARTESIAN_POINT('Ctrl Pts',(1.89500736899678,-0.489477875405323,
0.547709499817485));
#24364=CARTESIAN_POINT('Ctrl Pts',(1.73329672061383,-1.11555600193439,0.510672186384649));
#24365=CARTESIAN_POINT('Ctrl Pts',(1.23063940037359,-1.65352267851487,0.473634872951813));
#24366=CARTESIAN_POINT('Ctrl Pts',(0.616962143929708,-1.85738653188124,
0.436597559518977));
#24367=CARTESIAN_POINT('Ctrl Pts',(0.00328488748583246,-2.06125038524761,
0.399560246086142));
#24368=CARTESIAN_POINT('Ctrl Pts',(-0.721412305161677,-1.93101141539988,
0.362522932653306));
#24369=CARTESIAN_POINT('Ctrl Pts',(-1.2255735069054,-1.52604510705262,0.32548561922047));
#24370=CARTESIAN_POINT('Ctrl Pts',(-1.67757250343746,-1.1629779682701,0.29228031018839));
#24371=CARTESIAN_POINT('Ctrl Pts',(-1.95230952873461,-0.579091046852653,
0.25907500115631));
#24372=CARTESIAN_POINT('Ctrl Pts',(-1.95633598837559,0.00127248296362327,
0.22586969212423));
#24373=CARTESIAN_POINT('Ctrl Pts',(-1.95588590413641,0.00206796222160181,
0.124130307875766));
#24374=CARTESIAN_POINT('Ctrl Pts',(-1.95149442603296,-0.570486119123227,
0.156904012808695));
#24375=CARTESIAN_POINT('Ctrl Pts',(-1.68517377795595,-1.14821417361252,
0.189677717741624));
#24376=CARTESIAN_POINT('Ctrl Pts',(-1.24335992644724,-1.51202006337354,
0.222451422674553));
#24377=CARTESIAN_POINT('Ctrl Pts',(-0.74355823061328,-1.92357529197494,
0.259526659786979));
#24378=CARTESIAN_POINT('Ctrl Pts',(-0.0191734218330693,-2.06136888910912,
0.296601896899404));
#24379=CARTESIAN_POINT('Ctrl Pts',(0.59730918482247,-1.86366268614966,0.33367713401183));
#24380=CARTESIAN_POINT('Ctrl Pts',(1.21379179147801,-1.6659564831902,0.370752371124255));
#24381=CARTESIAN_POINT('Ctrl Pts',(1.72237219600888,-1.13275048013712,0.40782760823668));
#24382=CARTESIAN_POINT('Ctrl Pts',(1.89021021423941,-0.507705222320547,
0.444902845349105));
#24383=CARTESIAN_POINT('Ctrl Pts',(2.05804823246995,0.117340035496022,0.481978082461531));
#24384=CARTESIAN_POINT('Ctrl Pts',(1.88514386440015,0.834224548076076,0.519053319573957));
#24385=CARTESIAN_POINT('Ctrl Pts',(1.45061079828058,1.31401352267999,0.556128556686382));
#24386=CARTESIAN_POINT('Ctrl Pts',(1.01607773216101,1.7938024972839,0.593203793798808));
#24387=CARTESIAN_POINT('Ctrl Pts',(0.319915967991662,2.03649593391168,0.630279030911233));
#24388=CARTESIAN_POINT('Ctrl Pts',(-0.318741968595543,1.93105881108975,
0.667354268023658));
#24389=CARTESIAN_POINT('Ctrl Pts',(-0.95739990518275,1.82562168826782,0.704429505136084));
#24390=CARTESIAN_POINT('Ctrl Pts',(-1.53855401418781,1.37205400599619,0.74150474224851));
#24391=CARTESIAN_POINT('Ctrl Pts',(-1.79588703923712,0.778131328327298,
0.778579979360935));
#24392=CARTESIAN_POINT('Ctrl Pts',(-1.9012727786294,0.534901837996683,0.793763422199212));
#24393=CARTESIAN_POINT('Ctrl Pts',(-1.95234877280959,0.268132669686638,
0.808946865037489));
#24394=CARTESIAN_POINT('Ctrl Pts',(-1.95120671878141,0.000942122514504899,
0.824130307875766));
#24395=CARTESIAN_POINT('Origin',(0.,0.,0.));
#24396=CARTESIAN_POINT('',(-1.95279514498571,-0.00168107824419284,1.62586969212423));
#24397=CARTESIAN_POINT('',(-1.95278388634516,-0.00168888116712579,1.52413030787576));
#24398=CARTESIAN_POINT('',(-1.954,-2.39295984553393E-16,0.));
#24399=CARTESIAN_POINT('Ctrl Pts',(-1.95279514498571,-0.00168107824419284,
1.62586969212423));
#24400=CARTESIAN_POINT('Ctrl Pts',(-1.94903681723145,0.45580829851081,1.59981878225084));
#24401=CARTESIAN_POINT('Ctrl Pts',(-1.78858836662353,0.915672122197071,
1.57376787237745));
#24402=CARTESIAN_POINT('Ctrl Pts',(-1.49506049969948,1.26310357403151,1.54771696250405));
#24403=CARTESIAN_POINT('Ctrl Pts',(-1.07774365121422,1.75705666974124,1.51067964907122));
#24404=CARTESIAN_POINT('Ctrl Pts',(-0.391431901374392,2.02374896425016,
1.47364233563838));
#24405=CARTESIAN_POINT('Ctrl Pts',(0.249914641927464,1.94117972705521,1.43660502220554));
#24406=CARTESIAN_POINT('Ctrl Pts',(0.891261185229321,1.85861048986026,1.39956770877271));
#24407=CARTESIAN_POINT('Ctrl Pts',(1.48764252199321,1.42677972096142,1.36253039533987));
#24408=CARTESIAN_POINT('Ctrl Pts',(1.76623794405498,0.843232102738223,1.32549308190704));
#24409=CARTESIAN_POINT('Ctrl Pts',(2.04483336611675,0.25968448451502,1.2884557684742));
#24410=CARTESIAN_POINT('Ctrl Pts',(2.0056428734764,-0.475579983032552,1.25141845504136));
#24411=CARTESIAN_POINT('Ctrl Pts',(1.66659475578394,-1.02620605156362,1.21438114160853));
#24412=CARTESIAN_POINT('Ctrl Pts',(1.32754663809148,-1.57683212009468,1.17734382817569));
#24413=CARTESIAN_POINT('Ctrl Pts',(0.688640895346918,-1.94281978960923,
1.14030651474286));
#24414=CARTESIAN_POINT('Ctrl Pts',(0.0421509461412053,-1.956746580861,1.10326920131002));
#24415=CARTESIAN_POINT('Ctrl Pts',(-0.604339003064511,-1.97067337211277,
1.06623188787719));
#24416=CARTESIAN_POINT('Ctrl Pts',(-1.25841315873137,-1.63253928510176,
1.02919457444435));
#24417=CARTESIAN_POINT('Ctrl Pts',(-1.62085801283843,-1.09702287625329,
0.992157261011514));
#24418=CARTESIAN_POINT('Ctrl Pts',(-1.83708669330173,-0.777542532858632,
0.970061404715753));
#24419=CARTESIAN_POINT('Ctrl Pts',(-1.94952098456712,-0.38781143817112,
0.947965548419991));
#24420=CARTESIAN_POINT('Ctrl Pts',(-1.95128265771456,0.000979968443958618,
0.92586969212423));
#24421=CARTESIAN_POINT('Ctrl Pts',(-1.95120671878141,0.000942122514504899,
0.824130307875766));
#24422=CARTESIAN_POINT('Ctrl Pts',(-1.94956008223784,-0.384298600093132,
0.846022102149914));
#24423=CARTESIAN_POINT('Ctrl Pts',(-1.83936019485534,-0.770415304222176,
0.867913896424062));
#24424=CARTESIAN_POINT('Ctrl Pts',(-1.62687654459384,-1.08811501975669,
0.889805690698211));
#24425=CARTESIAN_POINT('Ctrl Pts',(-1.26702108380771,-1.62616101710563,
0.926880927810636));
#24426=CARTESIAN_POINT('Ctrl Pts',(-0.613798221141896,-1.96797533873735,
0.963956164923062));
#24427=CARTESIAN_POINT('Ctrl Pts',(0.0333981997247413,-1.95692658607738,
1.00103140203549));
#24428=CARTESIAN_POINT('Ctrl Pts',(0.680594620591375,-1.94587783341741,
1.03810663914791));
#24429=CARTESIAN_POINT('Ctrl Pts',(1.32176459965883,-1.58196600646575,1.07518187626034));
#24430=CARTESIAN_POINT('Ctrl Pts',(1.66305355512094,-1.03196363523784,1.11225711337276));
#24431=CARTESIAN_POINT('Ctrl Pts',(2.00434251058304,-0.481961264009935,
1.14933235048519));
#24432=CARTESIAN_POINT('Ctrl Pts',(2.04575044243979,0.254131651494222,1.18640758759761));
#24433=CARTESIAN_POINT('Ctrl Pts',(1.76829659796069,0.838942597907999,1.22348282471004));
#24434=CARTESIAN_POINT('Ctrl Pts',(1.49084275348159,1.42375354432178,1.26055806182247));
#24435=CARTESIAN_POINT('Ctrl Pts',(0.894527132666635,1.85728252164517,1.29763329893489));
#24436=CARTESIAN_POINT('Ctrl Pts',(0.252653428905354,1.94083943808002,1.33470853604732));
#24437=CARTESIAN_POINT('Ctrl Pts',(-0.389220274855925,2.02439635451486,
1.37178377315974));
#24438=CARTESIAN_POINT('Ctrl Pts',(-1.07665206156353,1.75798121006115,1.40885901027217));
#24439=CARTESIAN_POINT('Ctrl Pts',(-1.49458024744687,1.26369474377317,1.44593424738459));
#24440=CARTESIAN_POINT('Ctrl Pts',(-1.78840024024692,0.916191869184958,
1.47199960088165));
#24441=CARTESIAN_POINT('Ctrl Pts',(-1.94901418738241,0.456060303888852,
1.49806495437871));
#24442=CARTESIAN_POINT('Ctrl Pts',(-1.95278388634516,-0.00168888116712579,
1.52413030787576));
#24443=CARTESIAN_POINT('Origin',(0.,0.,0.));
#24444=CARTESIAN_POINT('',(-1.95720013100772,4.01036975386895E-5,2.32586969212423));
#24445=CARTESIAN_POINT('',(-1.95721475873132,-4.18937055542429E-5,2.22413030787576));
#24446=CARTESIAN_POINT('',(-1.954,-2.39295984553393E-16,0.));
#24447=CARTESIAN_POINT('Ctrl Pts',(-1.95720013100772,4.01036975387313E-5,
2.32586969212423));
#24448=CARTESIAN_POINT('Ctrl Pts',(-1.95720078041499,0.00218844021348119,
2.32574664294735));
#24449=CARTESIAN_POINT('Ctrl Pts',(-1.95719754885173,0.00433677471760079,
2.32562359377048));
#24450=CARTESIAN_POINT('Ctrl Pts',(-1.95719043044659,0.00648509634279326,
2.3255005445936));
#24451=CARTESIAN_POINT('Ctrl Pts',(-1.9550478187754,0.653121371426419,2.28846323116077));
#24452=CARTESIAN_POINT('Ctrl Pts',(-1.60076274017474,1.2985908336322,2.25142591772793));
#24453=CARTESIAN_POINT('Ctrl Pts',(-1.05640644317236,1.64761702679965,2.2143886042951));
#24454=CARTESIAN_POINT('Ctrl Pts',(-0.512050146169983,1.9966432199671,2.17735129086226));
#24455=CARTESIAN_POINT('Ctrl Pts',(0.22237736923411,2.04922614409623,2.14031397742942));
#24456=CARTESIAN_POINT('Ctrl Pts',(0.810904901655155,1.78131122209933,2.10327666399659));
#24457=CARTESIAN_POINT('Ctrl Pts',(1.3994324340762,1.51339630010242,2.06623935056375));
#24458=CARTESIAN_POINT('Ctrl Pts',(1.8420599835142,0.924983531979483,2.02920203713092));
#24459=CARTESIAN_POINT('Ctrl Pts',(1.9363031541186,0.285248202840816,1.99216472369808));
#24460=CARTESIAN_POINT('Ctrl Pts',(2.030546324723,-0.354487126297849,1.95512741026525));
#24461=CARTESIAN_POINT('Ctrl Pts',(1.7764051164938,-1.04554501645225,1.91809009683241));
#24462=CARTESIAN_POINT('Ctrl Pts',(1.29013896790468,-1.47179410874122,1.88105278339957));
#24463=CARTESIAN_POINT('Ctrl Pts',(0.80387281931556,-1.8980432010302,1.84401546996674));
#24464=CARTESIAN_POINT('Ctrl Pts',(0.0854817303665232,-2.05948349545377,
1.8069781565339));
#24465=CARTESIAN_POINT('Ctrl Pts',(-0.536399128085272,-1.88226256360254,
1.76994084310107));
#24466=CARTESIAN_POINT('Ctrl Pts',(-1.15827998653706,-1.70504163175131,
1.73290352966823));
#24467=CARTESIAN_POINT('Ctrl Pts',(-1.68365061449161,-1.18915947362529,
1.69586621623539));
#24468=CARTESIAN_POINT('Ctrl Pts',(-1.87217495490353,-0.570611446107024,
1.65882890280256));
#24469=CARTESIAN_POINT('Ctrl Pts',(-1.92809705865707,-0.387131122580406,
1.64784249924311));
#24470=CARTESIAN_POINT('Ctrl Pts',(-1.95438013781773,-0.194617253664394,
1.63685609568367));
#24471=CARTESIAN_POINT('Ctrl Pts',(-1.95279514498571,-0.00168107824419272,
1.62586969212423));
#24472=CARTESIAN_POINT('Ctrl Pts',(-1.95278388634516,-0.00168888116712579,
1.52413030787576));
#24473=CARTESIAN_POINT('Ctrl Pts',(-1.95437618958592,-0.19503999965723,
1.53514019149113));
#24474=CARTESIAN_POINT('Ctrl Pts',(-1.92798468468382,-0.387966059069047,
1.5461500751065));
#24475=CARTESIAN_POINT('Ctrl Pts',(-1.87182792927594,-0.571799497056349,
1.55715995872187));
#24476=CARTESIAN_POINT('Ctrl Pts',(-1.68272284016263,-1.19084948347563,
1.5942351958343));
#24477=CARTESIAN_POINT('Ctrl Pts',(-1.15608807687694,-1.70679166819193,
1.63131043294672));
#24478=CARTESIAN_POINT('Ctrl Pts',(-0.533290099975553,-1.88316099335306,
1.66838567005915));
#24479=CARTESIAN_POINT('Ctrl Pts',(0.0895078769258353,-2.05953031851418,
1.70546090717157));
#24480=CARTESIAN_POINT('Ctrl Pts',(0.808469067442917,-1.89632678412012,
1.742536144284));
#24481=CARTESIAN_POINT('Ctrl Pts',(1.2940806434107,-1.46834921584087,1.77961138139642));
#24482=CARTESIAN_POINT('Ctrl Pts',(1.77969221937849,-1.04037164756162,1.81668661850885));
#24483=CARTESIAN_POINT('Ctrl Pts',(2.03195418079698,-0.347620045397172,
1.85376185562127));
#24484=CARTESIAN_POINT('Ctrl Pts',(1.93525024356178,0.292404819142093,1.8908370927337));
#24485=CARTESIAN_POINT('Ctrl Pts',(1.83854630632657,0.932429683681362,1.92791232984612));
#24486=CARTESIAN_POINT('Ctrl Pts',(1.39287647043767,1.51972781059545,1.96498756695855));
#24487=CARTESIAN_POINT('Ctrl Pts',(0.802499325163421,1.78512991495868,2.00206280407098));
#24488=CARTESIAN_POINT('Ctrl Pts',(0.212122179889179,2.05053201932191,2.0391380411834));
#24489=CARTESIAN_POINT('Ctrl Pts',(-0.522962274770398,1.99403810113428,
2.07621327829583));
#24490=CARTESIAN_POINT('Ctrl Pts',(-1.06585153299182,1.64154030157863,2.11328851540825));
#24491=CARTESIAN_POINT('Ctrl Pts',(-1.60686689507973,1.29025922210662,2.15023577956409));
#24492=CARTESIAN_POINT('Ctrl Pts',(-1.95701157491646,0.645014173540876,
2.18718304371993));
#24493=CARTESIAN_POINT('Ctrl Pts',(-1.95721475873132,-4.18937055542428E-5,
2.22413030787576));
#24494=CARTESIAN_POINT('Origin',(0.,0.,0.));
#24495=CARTESIAN_POINT('',(-1.95267861104158,0.0016552724044671,3.02586969212423));
#24496=CARTESIAN_POINT('',(-1.95290774954615,0.00171310729769101,2.92413030787577));
#24497=CARTESIAN_POINT('',(-1.954,-2.39295984553393E-16,0.));
#24498=CARTESIAN_POINT('Ctrl Pts',(-1.95267861104158,0.0016552724044671,
3.02586969212423));
#24499=CARTESIAN_POINT('Ctrl Pts',(-1.95426730228936,0.198943040570848,
3.01463719021104));
#24500=CARTESIAN_POINT('Ctrl Pts',(-1.92676912869608,0.39579823972063,3.00340468829784));
#24501=CARTESIAN_POINT('Ctrl Pts',(-1.8683524720406,0.583005555161783,2.99217218638465));
#24502=CARTESIAN_POINT('Ctrl Pts',(-1.67573322844129,1.20029065090429,2.95513487295181));
#24503=CARTESIAN_POINT('Ctrl Pts',(-1.14695545989861,1.71267996796991,2.91809755951898));
#24504=CARTESIAN_POINT('Ctrl Pts',(-0.523913838219462,1.88577589531095,
2.88106024608614));
#24505=CARTESIAN_POINT('Ctrl Pts',(0.0991277834596942,2.05887182265199,
2.84402293265331));
#24506=CARTESIAN_POINT('Ctrl Pts',(0.816433258275323,1.89267436026844,2.80698561922047));
#24507=CARTESIAN_POINT('Ctrl Pts',(1.29986403215874,1.463212197494,2.76994830578763));
#24508=CARTESIAN_POINT('Ctrl Pts',(1.78329480604215,1.03375003471956,2.7329109923548));
#24509=CARTESIAN_POINT('Ctrl Pts',(2.03285087899336,0.341023171554252,2.69587367892196));
#24510=CARTESIAN_POINT('Ctrl Pts',(1.93437033276029,-0.298073569575231,
2.65883636548913));
#24511=CARTESIAN_POINT('Ctrl Pts',(1.83588978652722,-0.93717031070472,2.62179905205629));
#24512=CARTESIAN_POINT('Ctrl Pts',(1.38937262110987,-1.52263692979838,2.58476173862346));
#24513=CARTESIAN_POINT('Ctrl Pts',(0.799082573852251,-1.7866458736405,2.54772442519062));
#24514=CARTESIAN_POINT('Ctrl Pts',(0.208792526594628,-2.05065481748262,
2.51068711175778));
#24515=CARTESIAN_POINT('Ctrl Pts',(-0.525270402503268,-1.99320608607321,
2.47364979832495));
#24516=CARTESIAN_POINT('Ctrl Pts',(-1.06730179468137,-1.64058017638776,
2.43661248489211));
#24517=CARTESIAN_POINT('Ctrl Pts',(-1.60753239434872,-1.28912579681371,
2.39969822063615));
#24518=CARTESIAN_POINT('Ctrl Pts',(-1.95700531140595,-0.644452316926743,
2.36278395638019));
#24519=CARTESIAN_POINT('Ctrl Pts',(-1.95720013100772,4.01036975386895E-5,
2.32586969212423));
#24520=CARTESIAN_POINT('Ctrl Pts',(-1.95721475873132,-4.18937055544587E-5,
2.22413030787576));
#24521=CARTESIAN_POINT('Ctrl Pts',(-1.95721546249205,-0.00227615201876484,
2.22425828083235));
#24522=CARTESIAN_POINT('Ctrl Pts',(-1.9572119680126,-0.00451040806477065,
2.22438625378894));
#24523=CARTESIAN_POINT('Ctrl Pts',(-1.95720426868303,-0.00674464962048316,
2.22451422674553));
#24524=CARTESIAN_POINT('Ctrl Pts',(-1.95497368436953,-0.654030120340289,
2.26158946385795));
#24525=CARTESIAN_POINT('Ctrl Pts',(-1.59981845395926,-1.30009938085624,
2.29866470097038));
#24526=CARTESIAN_POINT('Ctrl Pts',(-1.0545126575596,-1.64884719787949,2.33573993808281));
#24527=CARTESIAN_POINT('Ctrl Pts',(-0.509206861159936,-1.99759501490274,
2.37281517519523));
#24528=CARTESIAN_POINT('Ctrl Pts',(0.226249501229124,-2.04902138843328,
2.40989041230765));
#24529=CARTESIAN_POINT('Ctrl Pts',(0.81478345819529,-1.77955667339696,2.44696564942008));
#24530=CARTESIAN_POINT('Ctrl Pts',(1.40331741516146,-1.51009195836063,2.4840408865325));
#24531=CARTESIAN_POINT('Ctrl Pts',(1.84492896670473,-0.919736154757425,
2.52111612364493));
#24532=CARTESIAN_POINT('Ctrl Pts',(1.93721953774244,-0.279060025103992,
2.55819136075736));
#24533=CARTESIAN_POINT('Ctrl Pts',(2.02951010878015,0.361616104549433,2.59526659786978));
#24534=CARTESIAN_POINT('Ctrl Pts',(1.7724796993123,1.05261256025308,2.63234183498221));
#24535=CARTESIAN_POINT('Ctrl Pts',(1.28393000274363,1.47723315072179,2.66941707209463));
#24536=CARTESIAN_POINT('Ctrl Pts',(0.795380306174951,1.9018537411905,2.70649230920706));
#24537=CARTESIAN_POINT('Ctrl Pts',(0.0753113225054439,2.06009846642426,
2.74356754631949));
#24538=CARTESIAN_POINT('Ctrl Pts',(-0.546256289304822,1.87944090130045,
2.78064278343191));
#24539=CARTESIAN_POINT('Ctrl Pts',(-1.16782390111508,1.69878333617665,2.81771802054433));
#24540=CARTESIAN_POINT('Ctrl Pts',(-1.6908901410661,1.17922348069528,2.85479325765676));
#24541=CARTESIAN_POINT('Ctrl Pts',(-1.875724275851,0.558885028961709,2.89186849476918));
#24542=CARTESIAN_POINT('Ctrl Pts',(-1.92933673865706,0.37895142411412,2.90262243247138));
#24543=CARTESIAN_POINT('Ctrl Pts',(-1.95449266845916,0.190538998342851,
2.91337637017357));
#24544=CARTESIAN_POINT('Ctrl Pts',(-1.95290774954615,0.00171310729769108,
2.92413030787576));
#24545=CARTESIAN_POINT('Origin',(0.,0.,0.));
#24546=CARTESIAN_POINT('',(-1.95135045472565,-0.00103665430809308,3.72586969212423));
#24547=CARTESIAN_POINT('',(-1.95115009645722,-0.000862413589311458,3.62413030787577));
#24548=CARTESIAN_POINT('',(-1.954,-2.39295984553393E-16,0.));
#24549=CARTESIAN_POINT('Ctrl Pts',(-1.95135045472565,-0.00103665430809308,
3.72586969212423));
#24550=CARTESIAN_POINT('Ctrl Pts',(-1.94945762145185,0.39205003232945,3.70352773747472));
#24551=CARTESIAN_POINT('Ctrl Pts',(-1.83432541049109,0.786156754205215,
3.6811857828252));
#24552=CARTESIAN_POINT('Ctrl Pts',(-1.61355237927334,1.1077387582254,3.65884382817569));
#24553=CARTESIAN_POINT('Ctrl Pts',(-1.2475664983152,1.64084043460512,3.62180651474286));
#24554=CARTESIAN_POINT('Ctrl Pts',(-0.591266345378013,1.97463505701166,
3.58476920131002));
#24555=CARTESIAN_POINT('Ctrl Pts',(0.0551170192794968,1.95642494139715,
3.54773188787719));
#24556=CARTESIAN_POINT('Ctrl Pts',(0.701500383937021,1.93821482578265,3.51069457444435));
#24557=CARTESIAN_POINT('Ctrl Pts',(1.33796696031487,1.56799997214707,3.47365726101151));
#24558=CARTESIAN_POINT('Ctrl Pts',(1.67335875584854,1.01513886309221,3.43661994757868));
#24559=CARTESIAN_POINT('Ctrl Pts',(2.00875055138221,0.46227775403734,3.39958263414584));
#24560=CARTESIAN_POINT('Ctrl Pts',(2.04306756607169,-0.273229610436822,
3.36254532071301));
#24561=CARTESIAN_POINT('Ctrl Pts',(1.76061113877997,-0.854918040011614,
3.32550800728017));
#24562=CARTESIAN_POINT('Ctrl Pts',(1.47815471148825,-1.4366064695864,3.28847069384734));
#24563=CARTESIAN_POINT('Ctrl Pts',(0.878924842215338,-1.86447596426182,
3.2514333804145));
#24564=CARTESIAN_POINT('Ctrl Pts',(0.237045219929842,-1.94279335001325,
3.21439606698166));
#24565=CARTESIAN_POINT('Ctrl Pts',(-0.404834402355659,-2.02111073576468,
3.17735875354883));
#24566=CARTESIAN_POINT('Ctrl Pts',(-1.08936377765374,-1.74987601259212,
3.14032144011599));
#24567=CARTESIAN_POINT('Ctrl Pts',(-1.50339810597481,-1.25316821379613,
3.10328412668316));
#24568=CARTESIAN_POINT('Ctrl Pts',(-1.79186605396357,-0.907099615934405,
3.07747931516352));
#24569=CARTESIAN_POINT('Ctrl Pts',(-1.94902885620257,-0.451580677342798,
3.05167450364387));
#24570=CARTESIAN_POINT('Ctrl Pts',(-1.95267861104158,0.0016552724044671,
3.02586969212423));
#24571=CARTESIAN_POINT('Ctrl Pts',(-1.95290774954615,0.00171310729769101,
2.92413030787577));
#24572=CARTESIAN_POINT('Ctrl Pts',(-1.94902850769025,-0.460456467442357,
2.950451607286));
#24573=CARTESIAN_POINT('Ctrl Pts',(-1.78495210853218,-0.925103000270984,
2.97677290669623));
#24574=CARTESIAN_POINT('Ctrl Pts',(-1.48583543343396,-1.27396510910143,
3.00309420610646));
#24575=CARTESIAN_POINT('Ctrl Pts',(-1.06451042661324,-1.76535974744522,
3.04016944321889));
#24576=CARTESIAN_POINT('Ctrl Pts',(-0.375258383353002,-2.02703197614702,
3.07724468033131));
#24577=CARTESIAN_POINT('Ctrl Pts',(0.266023999143107,-1.93905267245523,
3.11431991744374));
#24578=CARTESIAN_POINT('Ctrl Pts',(0.907306381639212,-1.85107336876345,
3.15139515455616));
#24579=CARTESIAN_POINT('Ctrl Pts',(1.50061910337119,-1.4134425326781,3.18847039166859));
#24580=CARTESIAN_POINT('Ctrl Pts',(1.77403619606301,-0.826734304146555,
3.22554562878102));
#24581=CARTESIAN_POINT('Ctrl Pts',(2.04745328875484,-0.240026075615009,
3.26262086589344));
#24582=CARTESIAN_POINT('Ctrl Pts',(2.0009747524065,0.495759545362725,3.29969610300586));
#24583=CARTESIAN_POINT('Ctrl Pts',(1.65590254220004,1.04339867994717,3.33677134011829));
#24584=CARTESIAN_POINT('Ctrl Pts',(1.31083033199357,1.59103781453161,3.37384657723071));
#24585=CARTESIAN_POINT('Ctrl Pts',(0.667164447928974,1.95053046272276,3.41092181434314));
#24586=CARTESIAN_POINT('Ctrl Pts',(0.0199086246964731,1.9571146316129,3.44799705145557));
#24587=CARTESIAN_POINT('Ctrl Pts',(-0.627347198536033,1.96369880050304,
3.485072288568));
#24588=CARTESIAN_POINT('Ctrl Pts',(-1.27819296093644,1.61737449009216,3.52214752568042));
#24589=CARTESIAN_POINT('Ctrl Pts',(-1.63433425949862,1.07686840552899,3.55922276279284));
#24590=CARTESIAN_POINT('Ctrl Pts',(-1.8421662177247,0.761447423909083,3.58085861115382));
#24591=CARTESIAN_POINT('Ctrl Pts',(-1.94963677903995,0.379897976317775,
3.60249445951479));
#24592=CARTESIAN_POINT('Ctrl Pts',(-1.95115009645722,-0.000862413589311458,
3.62413030787577));
#24593=CARTESIAN_POINT('Origin',(0.,0.,0.));
#24594=CARTESIAN_POINT('',(-1.95645463735042,-0.00107680116258307,4.42586969212423));
#24595=CARTESIAN_POINT('',(-1.9560689354221,-0.00131000797615835,4.32413030787576));
#24596=CARTESIAN_POINT('',(-1.954,-2.39295984553393E-16,0.));
#24597=CARTESIAN_POINT('Ctrl Pts',(-1.95645463735042,-0.00107680116258307,
4.42586969212423));
#24598=CARTESIAN_POINT('Ctrl Pts',(-1.95257837355362,0.583548870363389,
4.3924182847384));
#24599=CARTESIAN_POINT('Ctrl Pts',(-1.67319437992126,1.17138871222795,4.35896687735257));
#24600=CARTESIAN_POINT('Ctrl Pts',(-1.21542355114692,1.53407367113183,4.32551546996674));
#24601=CARTESIAN_POINT('Ctrl Pts',(-0.70858085032514,1.93563753794803,4.2884781565339));
#24602=CARTESIAN_POINT('Ctrl Pts',(0.0169438143861521,2.0611871352921,4.25144084310107));
#24603=CARTESIAN_POINT('Ctrl Pts',(0.629251938590984,1.85328854601076,4.21440352966823));
#24604=CARTESIAN_POINT('Ctrl Pts',(1.24156006279581,1.64538995672942,4.1773662162354));
#24605=CARTESIAN_POINT('Ctrl Pts',(1.74065164649418,1.10404318082267,4.14032890280256));
#24606=CARTESIAN_POINT('Ctrl Pts',(1.89821225955213,0.476892707953959,4.10329158936972));
#24607=CARTESIAN_POINT('Ctrl Pts',(2.05577287261007,-0.15025776491475,4.06625427593688));
#24608=CARTESIAN_POINT('Ctrl Pts',(1.87180251502759,-0.86321193474541,4.02921696250405));
#24609=CARTESIAN_POINT('Ctrl Pts',(1.4304602644841,-1.33582179532369,3.99217964907122));
#24610=CARTESIAN_POINT('Ctrl Pts',(0.989118013940611,-1.80843165590198,
3.95514233563838));
#24611=CARTESIAN_POINT('Ctrl Pts',(0.290403870436121,-2.04069720722789,
3.91810502220554));
#24612=CARTESIAN_POINT('Ctrl Pts',(-0.346048402169674,-1.92636625294191,
3.88106770877271));
#24613=CARTESIAN_POINT('Ctrl Pts',(-0.982500674775478,-1.81203529865592,
3.84403039533987));
#24614=CARTESIAN_POINT('Ctrl Pts',(-1.55669107648259,-1.35110783875803,
3.80699308190704));
#24615=CARTESIAN_POINT('Ctrl Pts',(-1.80595047284659,-0.754439743632632,
3.7699557684742));
#24616=CARTESIAN_POINT('Ctrl Pts',(-1.9048495538052,-0.517698713581134,
3.75526040969088));
#24617=CARTESIAN_POINT('Ctrl Pts',(-1.95259546056833,-0.259588333590661,
3.74056505090755));
#24618=CARTESIAN_POINT('Ctrl Pts',(-1.95135045472565,-0.00103665430809308,
3.72586969212423));
#24619=CARTESIAN_POINT('Ctrl Pts',(-1.95115009645722,-0.000862413589311458,
3.62413030787577));
#24620=CARTESIAN_POINT('Ctrl Pts',(-1.95223000307885,-0.272573861314833,
3.63956969662722));
#24621=CARTESIAN_POINT('Ctrl Pts',(-1.89935350538763,-0.543883498707529,
3.65500908537867));
#24622=CARTESIAN_POINT('Ctrl Pts',(-1.79048714938831,-0.790474416076489,
3.67044847413012));
#24623=CARTESIAN_POINT('Ctrl Pts',(-1.52906190599187,-1.38262329440335,
3.70752371124255));
#24624=CARTESIAN_POINT('Ctrl Pts',(-0.944774584475045,-1.83223319234163,
3.74459894835497));
#24625=CARTESIAN_POINT('Ctrl Pts',(-0.305414648672952,-1.93323974896447,
3.7816741854674));
#24626=CARTESIAN_POINT('Ctrl Pts',(0.333945287129141,-2.0342463055873,3.81874942257982));
#24627=CARTESIAN_POINT('Ctrl Pts',(1.0283778372165,-1.7866495208947,3.85582465969225));
#24628=CARTESIAN_POINT('Ctrl Pts',(1.45961198421181,-1.30392748653653,3.89289989680467));
#24629=CARTESIAN_POINT('Ctrl Pts',(1.89084613120712,-0.821205452178361,
3.9299751339171));
#24630=CARTESIAN_POINT('Ctrl Pts',(2.05888187511037,-0.103358168154617,
3.96705037102952));
#24631=CARTESIAN_POINT('Ctrl Pts',(1.88670539052006,0.520611951436678,4.00412560814195));
#24632=CARTESIAN_POINT('Ctrl Pts',(1.71452890592974,1.14458207102797,4.04120084525437));
#24633=CARTESIAN_POINT('Ctrl Pts',(1.20214019284586,1.67467502618682,4.0782760823668));
#24634=CARTESIAN_POINT('Ctrl Pts',(0.58437628040953,1.8679396129137,4.11535131947923));
#24635=CARTESIAN_POINT('Ctrl Pts',(-0.0333876320267997,2.06120419964058,
4.15242655659165));
#24636=CARTESIAN_POINT('Ctrl Pts',(-0.756526743815583,1.9176404179355,4.18950179370408));
#24637=CARTESIAN_POINT('Ctrl Pts',(-1.25361330032381,1.50304614961146,4.2265770308165));
#24638=CARTESIAN_POINT('Ctrl Pts',(-1.68959543059256,1.13941593283223,4.25909478983626));
#24639=CARTESIAN_POINT('Ctrl Pts',(-1.95168429546986,0.567292711935832,
4.29161254885601));
#24640=CARTESIAN_POINT('Ctrl Pts',(-1.9560689354221,-0.00131000797615835,
4.32413030787576));
#24641=CARTESIAN_POINT('Origin',(0.,0.,0.));
#24642=CARTESIAN_POINT('',(-1.95458552907139,0.00173412683576277,5.12586969212423));
#24643=CARTESIAN_POINT('',(-1.9552206747184,0.00161939276430114,5.02413030787577));
#24644=CARTESIAN_POINT('',(-1.954,-2.39295984553393E-16,0.));
#24645=CARTESIAN_POINT('Ctrl Pts',(-1.95458552907139,0.00173412683576277,
5.12586969212423));
#24646=CARTESIAN_POINT('Ctrl Pts',(-1.95579889273049,0.133549336413818,
5.11834614543492));
#24647=CARTESIAN_POINT('Ctrl Pts',(-1.94360248016884,0.265141296927549,
5.11082259874561));
#24648=CARTESIAN_POINT('Ctrl Pts',(-1.91717253101555,0.393809524200435,
5.10329905205629));
#24649=CARTESIAN_POINT('Ctrl Pts',(-1.78706177989932,1.02722427646379,5.06626173862345));
#24650=CARTESIAN_POINT('Ctrl Pts',(-1.31200866513269,1.58978387278703,5.02922442519062));
#24651=CARTESIAN_POINT('Ctrl Pts',(-0.709330998225857,1.82413979092323,
4.99218711175778));
#24652=CARTESIAN_POINT('Ctrl Pts',(-0.106653331319023,2.05849570905944,
4.95514979832495));
#24653=CARTESIAN_POINT('Ctrl Pts',(0.623648887728016,1.96464794900861,4.91811248489211));
#24654=CARTESIAN_POINT('Ctrl Pts',(1.14749162443816,1.58552811433593,4.88107517145928));
#24655=CARTESIAN_POINT('Ctrl Pts',(1.67133436114829,1.20640827966324,4.84403785802644));
#24656=CARTESIAN_POINT('Ctrl Pts',(1.98871761552153,0.542016370368706,4.8070005445936));
#24657=CARTESIAN_POINT('Ctrl Pts',(1.95445124244436,-0.103714902901561,
4.76996323116077));
#24658=CARTESIAN_POINT('Ctrl Pts',(1.9201848693672,-0.749446176171828,4.73292591772793));
#24659=CARTESIAN_POINT('Ctrl Pts',(1.53426886883963,-1.37651681341782,4.6958886042951));
#24660=CARTESIAN_POINT('Ctrl Pts',(0.973244372713117,-1.69806708597997,
4.65885129086226));
#24661=CARTESIAN_POINT('Ctrl Pts',(0.412219876586598,-2.01961735854213,
4.62181397742943));
#24662=CARTESIAN_POINT('Ctrl Pts',(-0.323913115138867,-2.03564726642044,
4.58477666399659));
#24663=CARTESIAN_POINT('Ctrl Pts',(-0.898403214163087,-1.7388237693533,
4.54773935056375));
#24664=CARTESIAN_POINT('Ctrl Pts',(-1.4728933131873,-1.44200027228616,4.51070203713092));
#24665=CARTESIAN_POINT('Ctrl Pts',(-1.88574051951028,-0.832323370273586,
4.47366472369808));
#24666=CARTESIAN_POINT('Ctrl Pts',(-1.94808375420563,-0.188695851123138,
4.43662741026525));
#24667=CARTESIAN_POINT('Ctrl Pts',(-1.95411974768256,-0.126380645212594,
4.43304150421824));
#24668=CARTESIAN_POINT('Ctrl Pts',(-1.95687016300016,-0.0637471906795113,
4.42945559817124));
#24669=CARTESIAN_POINT('Ctrl Pts',(-1.95645463735042,-0.00107680116258307,
4.42586969212423));
#24670=CARTESIAN_POINT('Ctrl Pts',(-1.9560689354221,-0.00131000797615835,
4.32413030787576));
#24671=CARTESIAN_POINT('Ctrl Pts',(-1.95668345810536,-0.0810016754695383,
4.32868778596844));
#24672=CARTESIAN_POINT('Ctrl Pts',(-1.95223589499426,-0.160624189738801,
4.33324526406111));
#24673=CARTESIAN_POINT('Ctrl Pts',(-1.94249551147141,-0.239593869899598,
4.33780274215378));
#24674=CARTESIAN_POINT('Ctrl Pts',(-1.86325716488311,-0.882014866143589,
4.3748779792662));
#24675=CARTESIAN_POINT('Ctrl Pts',(-1.43374647047883,-1.48123210368856,
4.41195321637863));
#24676=CARTESIAN_POINT('Ctrl Pts',(-0.850815960071711,-1.76261346774659,
4.44902845349105));
#24677=CARTESIAN_POINT('Ctrl Pts',(-0.267885449664584,-2.04399483180463,
4.48610369060348));
#24678=CARTESIAN_POINT('Ctrl Pts',(0.468464876745396,-2.00754032237573,
4.52317892771591));
#24679=CARTESIAN_POINT('Ctrl Pts',(1.02075232548754,-1.66995770146661,4.56025416482833));
#24680=CARTESIAN_POINT('Ctrl Pts',(1.57303977422969,-1.3323750805575,4.59732940194076));
#24681=CARTESIAN_POINT('Ctrl Pts',(1.941264345304,-0.693664348168167,4.63440463905318));
#24682=CARTESIAN_POINT('Ctrl Pts',(1.95666204750888,-0.0465582032952289,
4.67147987616561));
#24683=CARTESIAN_POINT('Ctrl Pts',(1.97205974971376,0.6005479415777,4.70855511327803));
#24684=CARTESIAN_POINT('Ctrl Pts',(1.63463058304921,1.25604949893424,4.74563035039046));
#24685=CARTESIAN_POINT('Ctrl Pts',(1.09902444690466,1.61951823074648,4.78270558750289));
#24686=CARTESIAN_POINT('Ctrl Pts',(0.56341831076011,1.98298696255872,4.81978082461531));
#24687=CARTESIAN_POINT('Ctrl Pts',(-0.170364794864445,2.05442286882665,
4.85685606172773));
#24688=CARTESIAN_POINT('Ctrl Pts',(-0.766018779707725,1.80108557937185,
4.89393129884016));
#24689=CARTESIAN_POINT('Ctrl Pts',(-1.361672764551,1.54774828991705,4.93100653595259));
#24690=CARTESIAN_POINT('Ctrl Pts',(-1.81919762861299,0.96963780473953,4.96808177306502));
#24691=CARTESIAN_POINT('Ctrl Pts',(-1.92890143946537,0.331712632206103,
5.00515701017744));
#24692=CARTESIAN_POINT('Ctrl Pts',(-1.9476151256888,0.222892971156397,5.01148144274355));
#24693=CARTESIAN_POINT('Ctrl Pts',(-1.95620763248682,0.112332773766476,
5.01780587530966));
#24694=CARTESIAN_POINT('Ctrl Pts',(-1.9552206747184,0.00161939276430114,
5.02413030787577));
#24695=CARTESIAN_POINT('Origin',(0.,0.,0.));
#24696=CARTESIAN_POINT('',(-1.95079790389112,-3.269510144494E-5,5.82586969212423));
#24697=CARTESIAN_POINT('',(-1.95085192255358,0.000383174536113729,5.72413030787576));
#24698=CARTESIAN_POINT('',(-1.954,-2.39295984553393E-16,0.));
#24699=CARTESIAN_POINT('Ctrl Pts',(-1.95079807093469,-3.26933958413878E-5,
5.82586969212423));
#24700=CARTESIAN_POINT('Ctrl Pts',(-1.95074883721548,0.328029941286317,
5.8072366926986));
#24701=CARTESIAN_POINT('Ctrl Pts',(-1.87242650231768,0.656114687980161,
5.78860369327296));
#24702=CARTESIAN_POINT('Ctrl Pts',(-1.71596284018057,0.941333347646706,
5.76997069384733));
#24703=CARTESIAN_POINT('Ctrl Pts',(-1.40495581640267,1.50827013831881,5.7329333804145));
#24704=CARTESIAN_POINT('Ctrl Pts',(-0.785207871169114,1.90584052998572,
5.69589606698167));
#24705=CARTESIAN_POINT('Ctrl Pts',(-0.140229809906548,1.95217121547304,
5.65885875354883));
#24706=CARTESIAN_POINT('Ctrl Pts',(0.504748251356019,1.99850190096035,5.62182144011599));
#24707=CARTESIAN_POINT('Ctrl Pts',(1.1749564286476,1.69359288026805,5.58478412668316));
#24708=CARTESIAN_POINT('Ctrl Pts',(1.56380177877164,1.17692822962597,5.54774681325032));
#24709=CARTESIAN_POINT('Ctrl Pts',(1.95264712889569,0.660263578983889,5.51070949981748));
#24710=CARTESIAN_POINT('Ctrl Pts',(2.06012965185219,-0.068156701607988,
5.47367218638465));
#24711=CARTESIAN_POINT('Ctrl Pts',(1.83708014107304,-0.675109688693547,
5.43663487295181));
#24712=CARTESIAN_POINT('Ctrl Pts',(1.61403063029389,-1.2820626757791,5.39959755951898));
#24713=CARTESIAN_POINT('Ctrl Pts',(1.06044908577908,-1.76754836935834,5.36256024608614));
#24714=CARTESIAN_POINT('Ctrl Pts',(0.429577047133733,-1.90947637973667,
5.32552293265331));
#24715=CARTESIAN_POINT('Ctrl Pts',(-0.201294991511623,-2.051404390115,5.28848561922047));
#24716=CARTESIAN_POINT('Ctrl Pts',(-0.909457524287529,-1.84977471729243,
5.25144830578764));
#24717=CARTESIAN_POINT('Ctrl Pts',(-1.37095459694257,-1.39682492677941,
5.2144109923548));
#24718=CARTESIAN_POINT('Ctrl Pts',(-1.73870581031982,-1.03588474984214,
5.18489722561128));
#24719=CARTESIAN_POINT('Ctrl Pts',(-1.94982568195559,-0.515357546731067,
5.15538345886775));
#24720=CARTESIAN_POINT('Ctrl Pts',(-1.95458552907139,0.00173412683576277,
5.12586969212423));
#24721=CARTESIAN_POINT('Ctrl Pts',(-1.9552206747184,0.00161939276430114,
5.02413030787577));
#24722=CARTESIAN_POINT('Ctrl Pts',(-1.95042186547898,-0.536693808344559,
5.05488111242208));
#24723=CARTESIAN_POINT('Ctrl Pts',(-1.71915285367837,-1.07862845650355,
5.0856319169684));
#24724=CARTESIAN_POINT('Ctrl Pts',(-1.32368315644793,-1.44172013107889,
5.11638272151471));
#24725=CARTESIAN_POINT('Ctrl Pts',(-0.846878304935377,-1.87948786194111,
5.15345795862714));
#24726=CARTESIAN_POINT('Ctrl Pts',(-0.131385844267519,-2.0572834637762,
5.19053319573957));
#24727=CARTESIAN_POINT('Ctrl Pts',(0.494871066573067,-1.89361998960963,
5.22760843285199));
#24728=CARTESIAN_POINT('Ctrl Pts',(1.12112797741365,-1.72995651544305,5.26468366996442));
#24729=CARTESIAN_POINT('Ctrl Pts',(1.65814933842698,-1.22483396527481,5.30175890707684));
#24730=CARTESIAN_POINT('Ctrl Pts',(1.85980853758091,-0.609759157741489,
5.33883414418927));
#24731=CARTESIAN_POINT('Ctrl Pts',(2.06146773673485,0.00531564979182955,
5.37590938130169));
#24732=CARTESIAN_POINT('Ctrl Pts',(1.9277647740294,0.730342714690214,5.41298461841412));
#24733=CARTESIAN_POINT('Ctrl Pts',(1.51997812810125,1.23302900604299,5.45005985552654));
#24734=CARTESIAN_POINT('Ctrl Pts',(1.11219148217311,1.73571529739576,5.48713509263897));
#24735=CARTESIAN_POINT('Ctrl Pts',(0.430321153022272,2.01606081520293,5.52421032975139));
#24736=CARTESIAN_POINT('Ctrl Pts',(-0.213119314048168,1.94557811718459,
5.56128556686382));
#24737=CARTESIAN_POINT('Ctrl Pts',(-0.856559781118622,1.87509541916625,
5.59836080397625));
#24738=CARTESIAN_POINT('Ctrl Pts',(-1.46157038610868,1.45378450532239,5.63543604108868));
#24739=CARTESIAN_POINT('Ctrl Pts',(-1.75086384963453,0.874739824296975,
5.6725112782011));
#24740=CARTESIAN_POINT('Ctrl Pts',(-1.88512280557994,0.606009472173862,
5.68971762142599));
#24741=CARTESIAN_POINT('Ctrl Pts',(-1.95138199037298,0.30330611490569,5.70692396465088));
#24742=CARTESIAN_POINT('Ctrl Pts',(-1.95085192255358,0.000383174536113729,
5.72413030787576));
#24743=CARTESIAN_POINT('Origin',(0.,0.,0.));
#24744=CARTESIAN_POINT('',(-1.95467666345581,-0.00169153748172557,6.52586969212423));
#24745=CARTESIAN_POINT('',(-1.95381346134878,-0.0017935399644829,6.42413030787577));
#24746=CARTESIAN_POINT('',(-1.954,-2.39295984553393E-16,0.));
#24747=CARTESIAN_POINT('Ctrl Pts',(-1.95467666345581,-0.00169153748172557,
6.52586969212423));
#24748=CARTESIAN_POINT('Ctrl Pts',(-1.94989845242835,0.519322657074601,
6.49612723996228));
#24749=CARTESIAN_POINT('Ctrl Pts',(-1.7351643372623,1.04378980187726,6.46638478780033));
#24750=CARTESIAN_POINT('Ctrl Pts',(-1.36233982826997,1.40523012754949,6.43664233563838));
#24751=CARTESIAN_POINT('Ctrl Pts',(-0.898073529048792,1.85532007158963,
6.39960502220555));
#24752=CARTESIAN_POINT('Ctrl Pts',(-0.188657797713761,2.05260571068844,
6.36256770877271));
#24753=CARTESIAN_POINT('Ctrl Pts',(0.441334197613014,1.90680041588618,6.32553039533987));
#24754=CARTESIAN_POINT('Ctrl Pts',(1.07132619293978,1.76099512108392,6.28849308190704));
#24755=CARTESIAN_POINT('Ctrl Pts',(1.62189445225829,1.2720988923806,6.2514557684742));
#24756=CARTESIAN_POINT('Ctrl Pts',(1.84119904752624,0.663781270447278,6.21441845504137));
#24757=CARTESIAN_POINT('Ctrl Pts',(2.06050364279419,0.055463648513944,6.17738114160853));
#24758=CARTESIAN_POINT('Ctrl Pts',(1.94854457401157,-0.672275366649399,
6.14034382817569));
#24759=CARTESIAN_POINT('Ctrl Pts',(1.556526550614,-1.18653430832568,6.10330651474286));
#24760=CARTESIAN_POINT('Ctrl Pts',(1.16450852721644,-1.70079325000195,6.06626920131002));
#24761=CARTESIAN_POINT('Ctrl Pts',(0.492431549203928,-2.00157211819116,
6.02923188787718));
#24762=CARTESIAN_POINT('Ctrl Pts',(-0.152249713101387,-1.9512713582857,
5.99219457444435));
#24763=CARTESIAN_POINT('Ctrl Pts',(-0.796930975406703,-1.90097059838025,
5.95515726101152));
#24764=CARTESIAN_POINT('Ctrl Pts',(-1.41421652200483,-1.49959021038012,
5.91811994757868));
#24765=CARTESIAN_POINT('Ctrl Pts',(-1.72172624414277,-0.930748421541415,
5.88108263414585));
#24766=CARTESIAN_POINT('Ctrl Pts',(-1.87453175193852,-0.648083672620247,
5.86267832013864));
#24767=CARTESIAN_POINT('Ctrl Pts',(-1.95084670040156,-0.324068969295429,
5.84427400613143));
#24768=CARTESIAN_POINT('Ctrl Pts',(-1.95079807093469,-3.26933958413878E-5,
5.82586969212423));
#24769=CARTESIAN_POINT('Ctrl Pts',(-1.95085192255358,0.000383174536113729,
5.72413030787576));
#24770=CARTESIAN_POINT('Ctrl Pts',(-1.95023983077328,-0.349414785416059,
5.7439992017633));
#24771=CARTESIAN_POINT('Ctrl Pts',(-1.86056894683247,-0.699505544060014,
5.76386809565083));
#24772=CARTESIAN_POINT('Ctrl Pts',(-1.68370318859703,-0.997916657928721,
5.78373698953837));
#24773=CARTESIAN_POINT('Ctrl Pts',(-1.35367274197203,-1.55475001092207,
5.82081222665079));
#24774=CARTESIAN_POINT('Ctrl Pts',(-0.7200355266604,-1.9316382687018,5.85788746376322));
#24775=CARTESIAN_POINT('Ctrl Pts',(-0.0731991044283191,-1.95584662548515,
5.89496270087565));
#24776=CARTESIAN_POINT('Ctrl Pts',(0.573637317803748,-1.9800549822685,5.93203793798808));
#24777=CARTESIAN_POINT('Ctrl Pts',(1.23367294695625,-1.65158343805548,5.9691131751005));
#24778=CARTESIAN_POINT('Ctrl Pts',(1.60440177887889,-1.12097662310535,6.00618841221292));
#24779=CARTESIAN_POINT('Ctrl Pts',(1.97513061080152,-0.590369808155209,
6.04326364932535));
#24780=CARTESIAN_POINT('Ctrl Pts',(2.05655264549427,0.142372277532039,6.08033888643777));
#24781=CARTESIAN_POINT('Ctrl Pts',(1.81135015364285,0.741420988743503,6.1174141235502));
#24782=CARTESIAN_POINT('Ctrl Pts',(1.56614766179142,1.34046969995497,6.15448936066263));
#24783=CARTESIAN_POINT('Ctrl Pts',(0.994320643395809,1.80582503669066,6.19156459777505));
#24784=CARTESIAN_POINT('Ctrl Pts',(0.357948800551169,1.92420559652088,6.22863983488748));
#24785=CARTESIAN_POINT('Ctrl Pts',(-0.278423042293462,2.04258615635109,
6.2657150719999));
#24786=CARTESIAN_POINT('Ctrl Pts',(-0.97933970958712,1.81399193927586,6.30279030911233));
#24787=CARTESIAN_POINT('Ctrl Pts',(-1.42356034057997,1.34319300038089,6.33986554622475));
#24788=CARTESIAN_POINT('Ctrl Pts',(-1.76010254058954,0.986515035416152,
6.36795380010842));
#24789=CARTESIAN_POINT('Ctrl Pts',(-1.9493114895094,0.49082125388787,6.3960420539921));
#24790=CARTESIAN_POINT('Ctrl Pts',(-1.95381346134878,-0.0017935399644829,
6.42413030787577));
#24791=CARTESIAN_POINT('Origin',(0.,0.,-1.2940562256037));
#24792=CARTESIAN_POINT('',(-1.55603866428123,-0.00134656425434549,6.75594377439631));
#24793=CARTESIAN_POINT('',(-1.55791343064937,0.000503462391539915,6.89405622560371));
#24794=CARTESIAN_POINT('',(-1.5555,-9.09151186476045E-14,-1.2940562256037));
#24795=CARTESIAN_POINT('',(-1.54730100999696,0.15949869736893,7.4445));
#24796=CARTESIAN_POINT('Ctrl Pts',(-1.55603866428123,-0.00134656425434554,
6.7559437743963));
#24797=CARTESIAN_POINT('Ctrl Pts',(-1.55697159855378,-0.103073339358787,
6.76323863566719));
#24798=CARTESIAN_POINT('Ctrl Pts',(-1.50153911503434,-0.720280229157285,
6.80757081037091));
#24799=CARTESIAN_POINT('Ctrl Pts',(-0.676946582872774,-1.70937536089767,
6.88894029850746));
#24800=CARTESIAN_POINT('Ctrl Pts',(1.06890459630572,-1.49565296874813,7.00005223880597));
#24801=CARTESIAN_POINT('Ctrl Pts',(1.83584092749207,0.0856835708872964,
7.11116417910447));
#24802=CARTESIAN_POINT('Ctrl Pts',(0.924965623038614,1.59014055343882,7.22227611940298));
#24803=CARTESIAN_POINT('Ctrl Pts',(-0.835858495286665,1.63675999125994,
7.33338805970149));
#24804=CARTESIAN_POINT('Ctrl Pts',(-1.49427628245053,0.673892957891604,
7.40746268656716));
#24805=CARTESIAN_POINT('Ctrl Pts',(-1.54730100999696,0.159498697368912,
7.4445));
#24806=CARTESIAN_POINT('',(-0.352169241380506,1.51510959188617,7.4445));
#24807=CARTESIAN_POINT('Origin',(0.,0.,7.4445));
#24808=CARTESIAN_POINT('Ctrl Pts',(-1.55791343064937,0.000503462391539858,
6.8940562256037));
#24809=CARTESIAN_POINT('Ctrl Pts',(-1.55587997194015,-0.488621135891717,
6.9292365352861));
#24810=CARTESIAN_POINT('Ctrl Pts',(-1.04365545248604,-1.49691459517969,
7.00149208208092));
#24811=CARTESIAN_POINT('Ctrl Pts',(0.672826183539381,-1.71093187207897,
7.11082286598819));
#24812=CARTESIAN_POINT('Ctrl Pts',(1.80435891657647,-0.361603954366771,
7.22204857732544));
#24813=CARTESIAN_POINT('Ctrl Pts',(1.27791236939833,1.32169962363241,7.33327428866273));
#24814=CARTESIAN_POINT('Ctrl Pts',(0.152038852759137,1.63230677878407,7.40742476288758));
#24815=CARTESIAN_POINT('Ctrl Pts',(-0.352169241380528,1.51510959188617,
7.44450000000001));
#24816=CARTESIAN_POINT('Origin',(0.,0.,-1.2940562256037));
#24817=CARTESIAN_POINT('',(-1.5529510743802,-2.6025883987463E-5,6.0559437743963));
#24818=CARTESIAN_POINT('',(-1.55535150415969,-0.0014277642860383,6.1940562256037));
#24819=CARTESIAN_POINT('',(-1.5555,-9.09151186476045E-14,-1.2940562256037));
#24820=CARTESIAN_POINT('Ctrl Pts',(-1.5529510743802,-2.60258839871949E-5,
6.0559437743963));
#24821=CARTESIAN_POINT('Ctrl Pts',(-1.55298978632273,-0.257978138044578,
6.07434808840351));
#24822=CARTESIAN_POINT('Ctrl Pts',(-1.36998122495718,-1.03498796260698,
6.12978971584355));
#24823=CARTESIAN_POINT('Ctrl Pts',(-0.143008426055117,-1.83280806515592,
6.2222686567164));
#24824=CARTESIAN_POINT('Ctrl Pts',(1.4620310918033,-1.11449456034272,6.33338059701493));
#24825=CARTESIAN_POINT('Ctrl Pts',(1.72940928754233,0.623475815429911,6.44449253731343));
#24826=CARTESIAN_POINT('Ctrl Pts',(0.414554230167772,1.79104708014026,6.55560447761194));
#24827=CARTESIAN_POINT('Ctrl Pts',(-1.16842639544942,1.35082658514471,6.65942155663957));
#24828=CARTESIAN_POINT('Ctrl Pts',(-1.55223492464296,0.413411664830818,
6.72620132223435));
#24829=CARTESIAN_POINT('Ctrl Pts',(-1.55603866428123,-0.00134656425434554,
6.7559437743963));
#24830=CARTESIAN_POINT('Ctrl Pts',(-1.55535150415969,-0.00142776428603842,
6.1940562256037));
#24831=CARTESIAN_POINT('Ctrl Pts',(-1.55649817143771,-0.126898399140172,
6.20304320883246));
#24832=CARTESIAN_POINT('Ctrl Pts',(-1.48522496230459,-0.768704224613979,
6.24910542917363));
#24833=CARTESIAN_POINT('Ctrl Pts',(-0.59667036110871,-1.73952595846347,
6.33224288662724));
#24834=CARTESIAN_POINT('Ctrl Pts',(1.13899278941852,-1.44381691390763,6.44346859796452));
#24835=CARTESIAN_POINT('Ctrl Pts',(1.83065601360088,0.17532136832598,6.5546943093018));
#24836=CARTESIAN_POINT('Ctrl Pts',(0.844193344579619,1.63380261073593,6.66592002063907));
#24837=CARTESIAN_POINT('Ctrl Pts',(-0.915934603694247,1.5945880622222,6.77714573197635));
#24838=CARTESIAN_POINT('Ctrl Pts',(-1.5455164129256,0.568558209121068,6.85319113363123));
#24839=CARTESIAN_POINT('Ctrl Pts',(-1.55802295943751,0.0268493253573782,
6.89216129817368));
#24840=CARTESIAN_POINT('Ctrl Pts',(-1.55791343064937,0.000503462391539858,
6.8940562256037));
#24841=CARTESIAN_POINT('Origin',(0.,0.,-1.2940562256037));
#24842=CARTESIAN_POINT('',(-1.555966115901,0.00138046790836748,5.3559437743963));
#24843=CARTESIAN_POINT('',(-1.55299394346576,0.000305029677950264,5.49405622560371));
#24844=CARTESIAN_POINT('',(-1.5555,-9.09151186476045E-14,-1.2940562256037));
#24845=CARTESIAN_POINT('Ctrl Pts',(-1.555966115901,0.00138046790836748,
5.3559437743963));
#24846=CARTESIAN_POINT('Ctrl Pts',(-1.55217699502656,-0.410255201607083,
5.38545754113982));
#24847=CARTESIAN_POINT('Ctrl Pts',(-1.17320681553292,-1.34462621114732,
5.45200862131617));
#24848=CARTESIAN_POINT('Ctrl Pts',(0.403496653242899,-1.79354886637635,
5.55559701492538));
#24849=CARTESIAN_POINT('Ctrl Pts',(1.72554797232085,-0.634122566945669,
5.66670895522387));
#24850=CARTESIAN_POINT('Ctrl Pts',(1.46886056527041,1.10547479200108,5.77782089552239));
#24851=CARTESIAN_POINT('Ctrl Pts',(-0.131715923640121,1.83365183655613,
5.88893283582089));
#24852=CARTESIAN_POINT('Ctrl Pts',(-1.36662941760285,1.04145067599478,5.9816404621122));
#24853=CARTESIAN_POINT('Ctrl Pts',(-1.55291188141693,0.261131306893961,
6.03731077497067));
#24854=CARTESIAN_POINT('Ctrl Pts',(-1.5529510743802,-2.60258839871949E-5,
6.0559437743963));
#24855=CARTESIAN_POINT('Ctrl Pts',(-1.55299394346576,0.000305029677950229,
5.49405622560371));
#24856=CARTESIAN_POINT('Ctrl Pts',(-1.55250668207154,-0.278154912341265,
5.51392511949124));
#24857=CARTESIAN_POINT('Ctrl Pts',(-1.34792243677793,-1.07688746067556,
5.5708692504912));
#24858=CARTESIAN_POINT('Ctrl Pts',(-0.0687781849042931,-1.83772416168987,
5.66488861860358));
#24859=CARTESIAN_POINT('Ctrl Pts',(1.50750444735784,-1.05327561457109,5.77611432994086));
#24860=CARTESIAN_POINT('Ctrl Pts',(1.70195476716013,0.696642984640571,5.88734004127814));
#24861=CARTESIAN_POINT('Ctrl Pts',(0.336330007005007,1.80799440678846,5.99856575261541));
#24862=CARTESIAN_POINT('Ctrl Pts',(-1.20233240386818,1.30618107352199,6.10080448072394));
#24863=CARTESIAN_POINT('Ctrl Pts',(-1.55176766731418,0.390722855896857,
6.16596797172003));
#24864=CARTESIAN_POINT('Ctrl Pts',(-1.55535150415969,-0.00142776428603842,
6.1940562256037));
#24865=CARTESIAN_POINT('Origin',(0.,0.,-1.2940562256037));
#24866=CARTESIAN_POINT('',(-1.55745403705147,-0.000857197650203868,4.6559437743963));
#24867=CARTESIAN_POINT('',(-1.55647172954169,0.00128913277620515,4.7940562256037));
#24868=CARTESIAN_POINT('',(-1.5555,-9.09151186476045E-14,-1.2940562256037));
#24869=CARTESIAN_POINT('Ctrl Pts',(-1.55745403705147,-0.000857197650203714,
4.6559437743963));
#24870=CARTESIAN_POINT('Ctrl Pts',(-1.55778482013651,-0.0507465481586787,
4.6595296804433));
#24871=CARTESIAN_POINT('Ctrl Pts',(-1.5329809661149,-0.615588902391355,
4.70015289992314));
#24872=CARTESIAN_POINT('Ctrl Pts',(-0.843859631129698,-1.63325682938675,
4.77781343283583));
#24873=CARTESIAN_POINT('Ctrl Pts',(0.914157055608714,-1.59497455450745,
4.88892537313433));
#24874=CARTESIAN_POINT('Ctrl Pts',(1.83579319504673,-0.0974181938582904,
5.00003731343284));
#24875=CARTESIAN_POINT('Ctrl Pts',(1.07782545884778,1.48926801121999,5.11114925373134));
#24876=CARTESIAN_POINT('Ctrl Pts',(-0.666266304296033,1.713393176152,5.22226119402985));
#24877=CARTESIAN_POINT('Ctrl Pts',(-1.49942664147989,0.726761727184559,
5.30385936758484));
#24878=CARTESIAN_POINT('Ctrl Pts',(-1.55693202540547,0.106313199995716,
5.34842022770699));
#24879=CARTESIAN_POINT('Ctrl Pts',(-1.555966115901,0.00138046790836748,
5.3559437743963));
#24880=CARTESIAN_POINT('Ctrl Pts',(-1.55647172954169,0.00128913277620508,
4.7940562256037));
#24881=CARTESIAN_POINT('Ctrl Pts',(-1.55265159250384,-0.427240132487249,
4.82480703015002));
#24882=CARTESIAN_POINT('Ctrl Pts',(-1.14657973682021,-1.37879177584745,
4.89263307180876));
#24883=CARTESIAN_POINT('Ctrl Pts',(0.464983542380115,-1.77925562259896,
4.99753435057992));
#24884=CARTESIAN_POINT('Ctrl Pts',(1.74748619395055,-0.572933012383953,
5.1087600619172));
#24885=CARTESIAN_POINT('Ctrl Pts',(1.42817970701863,1.15856074316792,5.21998577325448));
#24886=CARTESIAN_POINT('Ctrl Pts',(-0.20024807751692,1.82807576816643,5.33121148459175));
#24887=CARTESIAN_POINT('Ctrl Pts',(-1.38701509520349,1.00164745002229,5.4225683020415));
#24888=CARTESIAN_POINT('Ctrl Pts',(-1.55341590891771,0.24144967335499,5.47684988237881));
#24889=CARTESIAN_POINT('Ctrl Pts',(-1.55299394346576,0.000305029677950229,
5.49405622560371));
#24890=CARTESIAN_POINT('Origin',(0.,0.,-1.2940562256037));
#24891=CARTESIAN_POINT('',(-1.55339080467029,-0.000825238370695906,3.9559437743963));
#24892=CARTESIAN_POINT('',(-1.55714699541918,-0.00104284411826,4.0940562256037));
#24893=CARTESIAN_POINT('',(-1.5555,-9.09151186476045E-14,-1.2940562256037));
#24894=CARTESIAN_POINT('Ctrl Pts',(-1.55339080467029,-0.000825238370696021,
3.9559437743963));
#24895=CARTESIAN_POINT('Ctrl Pts',(-1.55438190323133,-0.206647724104582,
3.97063913317962));
#24896=CARTESIAN_POINT('Ctrl Pts',(-1.42057875865067,-0.929976336606789,
4.02237180539578));
#24897=CARTESIAN_POINT('Ctrl Pts',(-0.325039216866852,-1.80941329116195,
4.11114179104478));
#24898=CARTESIAN_POINT('Ctrl Pts',(1.34361459616473,-1.25472178898058,4.22225373134328));
#24899=CARTESIAN_POINT('Ctrl Pts',(1.78296857449566,0.447939743012656,4.3333656716418));
#24900=CARTESIAN_POINT('Ctrl Pts',(0.591048986302979,1.74077225568864,4.44447761194029));
#24901=CARTESIAN_POINT('Ctrl Pts',(-1.08571442614287,1.45061399985919,4.5520036461918));
#24902=CARTESIAN_POINT('Ctrl Pts',(-1.55436830095327,0.464539543423835,
4.62249236701046));
#24903=CARTESIAN_POINT('Ctrl Pts',(-1.55745403705147,-0.000857197650203714,
4.6559437743963));
#24904=CARTESIAN_POINT('Ctrl Pts',(-1.55714699541918,-0.00104284411826003,
4.0940562256037));
#24905=CARTESIAN_POINT('Ctrl Pts',(-1.55763619195644,-0.0644821423710283,
4.09861370369637));
#24906=CARTESIAN_POINT('Ctrl Pts',(-1.52529338404343,-0.643499375005814,
4.14024641890147));
#24907=CARTESIAN_POINT('Ctrl Pts',(-0.799431294618187,-1.65616118233816,
4.21895437121899));
#24908=CARTESIAN_POINT('Ctrl Pts',(0.959104426053338,-1.56910132141185,
4.33018008255627));
#24909=CARTESIAN_POINT('Ctrl Pts',(1.83849028118038,-0.0437463405035559,
4.44140579389354));
#24910=CARTESIAN_POINT('Ctrl Pts',(1.0326493363287,1.52170812080878,4.55263150523082));
#24911=CARTESIAN_POINT('Ctrl Pts',(-0.719755403894915,1.69230978744094,
4.6638572165681));
#24912=CARTESIAN_POINT('Ctrl Pts',(-1.51031879937117,0.693384867678679,
4.74433212335906));
#24913=CARTESIAN_POINT('Ctrl Pts',(-1.55725740651651,0.0894235565985826,
4.78773179303759));
#24914=CARTESIAN_POINT('Ctrl Pts',(-1.55647172954169,0.00128913277620508,
4.7940562256037));
#24915=CARTESIAN_POINT('Origin',(0.,0.,-1.2940562256037));
#24916=CARTESIAN_POINT('',(-1.55444809594431,0.00131769509984214,3.2559437743963));
#24917=CARTESIAN_POINT('',(-1.55323130759427,-0.000686532414708174,3.3940562256037));
#24918=CARTESIAN_POINT('',(-1.5555,-9.09151186476045E-14,-1.2940562256037));
#24919=CARTESIAN_POINT('Ctrl Pts',(-1.55444809594431,0.00131769509984224,
3.2559437743963));
#24920=CARTESIAN_POINT('Ctrl Pts',(-1.55154267442328,-0.359485027434377,
3.28174858591594));
#24921=CARTESIAN_POINT('Ctrl Pts',(-1.24686166172698,-1.24256912580371,
3.34459071086842));
#24922=CARTESIAN_POINT('Ctrl Pts',(0.222653802667342,-1.82484307132901,
3.44447014925373));
#24923=CARTESIAN_POINT('Ctrl Pts',(1.65372145106143,-0.803014516107455,
3.55558208955224));
#24924=CARTESIAN_POINT('Ctrl Pts',(1.57176630825256,0.953508061332994,3.66669402985075));
#24925=CARTESIAN_POINT('Ctrl Pts',(0.0517707715753711,1.83764706567811,
3.77780597014925));
#24926=CARTESIAN_POINT('Ctrl Pts',(-1.30829594910608,1.14591637592306,3.87422255166444));
#24927=CARTESIAN_POINT('Ctrl Pts',(-1.55188399701554,0.312095099942876,
3.93360181974679));
#24928=CARTESIAN_POINT('Ctrl Pts',(-1.55339080467029,-0.000825238370696021,
3.9559437743963));
#24929=CARTESIAN_POINT('Ctrl Pts',(-1.55323130759427,-0.000686532414707983,
3.3940562256037));
#24930=CARTESIAN_POINT('Ctrl Pts',(-1.55409097737417,-0.216984975064148,
3.40949561435515));
#24931=CARTESIAN_POINT('Ctrl Pts',(-1.4109189051218,-0.95160176519996,3.46201024021903));
#24932=CARTESIAN_POINT('Ctrl Pts',(-0.286969261786828,-1.81648256240041,
3.55160010319533));
#24933=CARTESIAN_POINT('Ctrl Pts',(1.37145934362907,-1.22517734450477,3.66282581453261));
#24934=CARTESIAN_POINT('Ctrl Pts',(1.77275862659963,0.489169815626649,3.77405152586988));
#24935=CARTESIAN_POINT('Ctrl Pts',(0.549083125265984,1.75512620009375,3.88527723720716));
#24936=CARTESIAN_POINT('Ctrl Pts',(-1.10713858120128,1.42631885494224,3.99194547045177));
#24937=CARTESIAN_POINT('Ctrl Pts',(-1.5536565617213,0.451598676262059,4.06153846658395));
#24938=CARTESIAN_POINT('Ctrl Pts',(-1.55714699541918,-0.00104284411826003,
4.0940562256037));
#24939=CARTESIAN_POINT('Origin',(0.,0.,-1.2940562256037));
#24940=CARTESIAN_POINT('',(-1.55804749425921,3.19249239839854E-5,2.5559437743963));
#24941=CARTESIAN_POINT('',(-1.55463050379685,0.00136373510819555,2.6940562256037));
#24942=CARTESIAN_POINT('',(-1.5555,-9.09151186476045E-14,-1.2940562256037));
#24943=CARTESIAN_POINT('Ctrl Pts',(-1.55804749425921,3.19249239839832E-5,
2.5559437743963));
#24944=CARTESIAN_POINT('Ctrl Pts',(-1.55789240629065,-0.513022302446059,
2.59285803865226));
#24945=CARTESIAN_POINT('Ctrl Pts',(-1.00056267955874,-1.54112970888597,
2.66680961634105));
#24946=CARTESIAN_POINT('Ctrl Pts',(0.750568915726592,-1.67817557333754,
2.77779850746269));
#24947=CARTESIAN_POINT('Ctrl Pts',(1.81693142975936,-0.279977017554228,
2.8889104477612));
#24948=CARTESIAN_POINT('Ctrl Pts',(1.22094708256035,1.37437810371544,3.0000223880597));
#24949=CARTESIAN_POINT('Ctrl Pts',(-0.492106140687917,1.77128724302598,
3.11113432835821));
#24950=CARTESIAN_POINT('Ctrl Pts',(-1.46164337385231,0.831798954515017,
3.19644145713707));
#24951=CARTESIAN_POINT('Ctrl Pts',(-1.55571278849084,0.158370470628406,
3.2447112724831));
#24952=CARTESIAN_POINT('Ctrl Pts',(-1.55444809594431,0.00131769509984224,
3.2559437743963));
#24953=CARTESIAN_POINT('Ctrl Pts',(-1.55463050379685,0.0013637351081955,
2.6940562256037));
#24954=CARTESIAN_POINT('Ctrl Pts',(-1.55154239698677,-0.366550683268523,
2.72037752501393));
#24955=CARTESIAN_POINT('Ctrl Pts',(-1.23694887232287,-1.2574453593796,2.78377406153659));
#24956=CARTESIAN_POINT('Ctrl Pts',(0.249957593646744,-1.82194441691009,
2.88424583517168));
#24957=CARTESIAN_POINT('Ctrl Pts',(1.6668940398915,-0.776804039943688,2.99547154650895));
#24958=CARTESIAN_POINT('Ctrl Pts',(1.55589501744036,0.980383063583733,3.10669725784622));
#24959=CARTESIAN_POINT('Ctrl Pts',(0.0187062518377651,1.83891553174339,
3.2179229691835));
#24960=CARTESIAN_POINT('Ctrl Pts',(-1.31986995326957,1.12664004660162,3.31370929176933));
#24961=CARTESIAN_POINT('Ctrl Pts',(-1.55202661709144,0.302421341945843,
3.37242037724273));
#24962=CARTESIAN_POINT('Ctrl Pts',(-1.55323130759427,-0.000686532414707983,
3.3940562256037));
#24963=CARTESIAN_POINT('Origin',(0.,0.,-1.2940562256037));
#24964=CARTESIAN_POINT('',(-1.55454086388192,-0.001338238080313,1.8559437743963));
#24965=CARTESIAN_POINT('',(-1.55805913879558,-3.33498767488005E-5,1.9940562256037));
#24966=CARTESIAN_POINT('',(-1.5555,-9.09151186476045E-14,-1.2940562256037));
#24967=CARTESIAN_POINT('Ctrl Pts',(-1.55454086388192,-0.00133823808031298,
1.8559437743963));
#24968=CARTESIAN_POINT('Ctrl Pts',(-1.55580261226994,-0.154926887448841,
1.86693017795574));
#24969=CARTESIAN_POINT('Ctrl Pts',(-1.46434456543453,-0.824823376066396,
1.91495389494802));
#24970=CARTESIAN_POINT('Ctrl Pts',(-0.503833422351614,-1.76798718278107,
2.00001492537314));
#24971=CARTESIAN_POINT('Ctrl Pts',(1.211812440791,-1.38243900779253,2.11112686567164));
#24972=CARTESIAN_POINT('Ctrl Pts',(1.81874690762903,0.2679303086893,2.22223880597015));
#24973=CARTESIAN_POINT('Ctrl Pts',(0.761673489280804,1.67316479305249,2.33335074626865));
#24974=CARTESIAN_POINT('Ctrl Pts',(-0.99227021626331,1.54758740541246,2.44446268656716));
#24975=CARTESIAN_POINT('Ctrl Pts',(-1.5572711215541,0.518216278848874,2.51866036260971));
#24976=CARTESIAN_POINT('Ctrl Pts',(-1.55804801122595,0.00174212832754369,
2.55582072521942));
#24977=CARTESIAN_POINT('Ctrl Pts',(-1.55804749425921,3.19249239839832E-5,
2.5559437743963));
#24978=CARTESIAN_POINT('Ctrl Pts',(-1.55805913879558,-3.33498767486382E-5,
1.9940562256037));
#24979=CARTESIAN_POINT('Ctrl Pts',(-1.5580596990309,-0.00181195213168648,
1.99418419856029));
#24980=CARTESIAN_POINT('Ctrl Pts',(-1.5572509939767,-0.518871555499298,
2.0313874086293));
#24981=CARTESIAN_POINT('Ctrl Pts',(-0.990825815880477,-1.5492657736205,
2.10566585581074));
#24982=CARTESIAN_POINT('Ctrl Pts',(0.765574959497512,-1.6720811124538,2.21689156714802));
#24983=CARTESIAN_POINT('Ctrl Pts',(1.82022199392772,-0.262206313316451,
2.32811727848529));
#24984=CARTESIAN_POINT('Ctrl Pts',(1.20638759997596,1.38801628675575,2.43934298982257));
#24985=CARTESIAN_POINT('Ctrl Pts',(-0.513265374585843,1.76593287340023,
2.55056870115984));
#24986=CARTESIAN_POINT('Ctrl Pts',(-1.46682634638563,0.818764115677731,
2.63547311308689));
#24987=CARTESIAN_POINT('Ctrl Pts',(-1.55589219334096,0.151680354105525,
2.68330228790151));
#24988=CARTESIAN_POINT('Ctrl Pts',(-1.55463050379685,0.0013637351081955,
2.6940562256037));
#24989=CARTESIAN_POINT('Origin',(0.,0.,-1.2940562256037));
#24990=CARTESIAN_POINT('',(-1.55333683422467,0.00078011305757314,1.1559437743963));
#24991=CARTESIAN_POINT('',(-1.55453190133567,-0.00134444967022529,1.2940562256037));
#24992=CARTESIAN_POINT('',(-1.5555,-9.09151186476045E-14,-1.2940562256037));
#24993=CARTESIAN_POINT('Ctrl Pts',(-1.55333683422467,0.000780113057573043,
1.1559437743963));
#24994=CARTESIAN_POINT('Ctrl Pts',(-1.55193443781686,-0.308720927367064,
1.17803963069206));
#24995=CARTESIAN_POINT('Ctrl Pts',(-1.31240187276934,-1.13901289380036,
1.23717280042066));
#24996=CARTESIAN_POINT('Ctrl Pts',(0.0395921340189295,-1.83794780075079,
1.33334328358209));
#24997=CARTESIAN_POINT('Ctrl Pts',(1.56541283438613,-0.96390406493211,1.44445522388059));
#24998=CARTESIAN_POINT('Ctrl Pts',(1.65900671048959,0.792038431388639,1.55556716417911));
#24999=CARTESIAN_POINT('Ctrl Pts',(0.234741865039883,1.82332721494359,1.66667910447761));
#25000=CARTESIAN_POINT('Ctrl Pts',(-1.24223016373737,1.24939407250205,1.76680464121668));
#25001=CARTESIAN_POINT('Ctrl Pts',(-1.55154901187489,0.362850464858491,
1.8298928645229));
#25002=CARTESIAN_POINT('Ctrl Pts',(-1.55454086388192,-0.00133823808031298,
1.8559437743963));
#25003=CARTESIAN_POINT('Ctrl Pts',(-1.55453190133567,-0.00134444967022513,
1.2940562256037));
#25004=CARTESIAN_POINT('Ctrl Pts',(-1.55579946924303,-0.155263418355649,
1.30506610921907));
#25005=CARTESIAN_POINT('Ctrl Pts',(-1.46404280977096,-0.826019057429759,
1.35315122994686));
#25006=CARTESIAN_POINT('Ctrl Pts',(-0.501082205369057,-1.76942810040879,
1.43831158778708));
#25007=CARTESIAN_POINT('Ctrl Pts',(1.21592516185098,-1.37966899434435,1.54953729912436));
#25008=CARTESIAN_POINT('Ctrl Pts',(1.8183716526183,0.274745208061178,1.66076301046163));
#25009=CARTESIAN_POINT('Ctrl Pts',(0.754032712405612,1.67731773070425,1.77198872179891));
#25010=CARTESIAN_POINT('Ctrl Pts',(-0.999460041113845,1.5425554247787,1.8830864601796));
#25011=CARTESIAN_POINT('Ctrl Pts',(-1.5578973924169,0.513469573665662,1.95710896144786));
#25012=CARTESIAN_POINT('Ctrl Pts',(-1.55805913879558,-3.33498767486382E-5,
1.9940562256037));
#25013=CARTESIAN_POINT('Origin',(0.,0.,-1.2940562256037));
#25014=CARTESIAN_POINT('',(-1.55735958542387,0.00101297198046619,0.455943774396298));
#25015=CARTESIAN_POINT('',(-1.55327638232574,0.000749985450956003,0.594056225603703));
#25016=CARTESIAN_POINT('',(-1.5555,-9.09151186476045E-14,-1.2940562256037));
#25017=CARTESIAN_POINT('Ctrl Pts',(-1.55735958542387,0.00101297198046621,
0.455943774396298));
#25018=CARTESIAN_POINT('Ctrl Pts',(-1.55415428451722,-0.460990851268869,
0.489149083428377));
#25019=CARTESIAN_POINT('Ctrl Pts',(-1.09150079880486,-1.44424863810505,
0.559391705893293));
#25020=CARTESIAN_POINT('Ctrl Pts',(0.579516952736672,-1.74455562530747,
0.666671641791043));
#25021=CARTESIAN_POINT('Ctrl Pts',(1.77995215483547,-0.45979539180552,0.777783582089551));
#25022=CARTESIAN_POINT('Ctrl Pts',(1.35190460952174,1.24581651128198,0.888895522388059));
#25023=CARTESIAN_POINT('Ctrl Pts',(-0.313043761712607,1.81151378121076,
1.00000746268657));
#25024=CARTESIAN_POINT('Ctrl Pts',(-1.41743746237044,0.936955068058493,
1.08902354668931));
#25025=CARTESIAN_POINT('Ctrl Pts',(-1.55428514985164,0.21006806585223,1.14100231725922));
#25026=CARTESIAN_POINT('Ctrl Pts',(-1.55333683422467,0.000780113057573043,
1.1559437743963));
#25027=CARTESIAN_POINT('Ctrl Pts',(-1.55327638232574,0.000749985450955847,
0.594056225603703));
#25028=CARTESIAN_POINT('Ctrl Pts',(-1.55196556188379,-0.305924499715954,
0.61594801987785));
#25029=CARTESIAN_POINT('Ctrl Pts',(-1.3156705723219,-1.13385132195631,0.674915051264423));
#25030=CARTESIAN_POINT('Ctrl Pts',(0.0313843551128396,-1.83872969125081,
0.770957319763422));
#25031=CARTESIAN_POINT('Ctrl Pts',(1.56261245507102,-0.969643437172017,
0.882183031100698));
#25032=CARTESIAN_POINT('Ctrl Pts',(1.66150197094076,0.788277540412492,0.993408742437974));
#25033=CARTESIAN_POINT('Ctrl Pts',(0.237394066880885,1.82362194812979,1.10463445377525));
#25034=CARTESIAN_POINT('Ctrl Pts',(-1.24180780125352,1.25035520807598,1.20485028149716));
#25035=CARTESIAN_POINT('Ctrl Pts',(-1.55153099717163,0.363051076099792,
1.26799087210664));
#25036=CARTESIAN_POINT('Ctrl Pts',(-1.55453190133567,-0.00134444967022513,
1.2940562256037));
#25037=CARTESIAN_POINT('Origin',(0.,0.,7.5));
#25038=CARTESIAN_POINT('',(-1.90714972453263,0.000559583190138325,7.09553262944276));
#25039=CARTESIAN_POINT('Ctrl Pts',(-0.352169241380463,1.51510959188618,
7.4445));
#25040=CARTESIAN_POINT('Ctrl Pts',(-0.294581668876612,1.53128067531421,
7.44178679402676));
#25041=CARTESIAN_POINT('Ctrl Pts',(-0.236177221040451,1.54382025621514,
7.43908623010619));
#25042=CARTESIAN_POINT('Ctrl Pts',(-0.17725379571509,1.55288079770358,7.43639376053775));
#25043=CARTESIAN_POINT('Ctrl Pts',(-0.119240420394871,1.56180140255761,
7.43374287514286));
#25044=CARTESIAN_POINT('Ctrl Pts',(-0.0607231436400752,1.56734934022223,
7.4310998360025));
#25045=CARTESIAN_POINT('Ctrl Pts',(-0.00197185718845893,1.56962582506071,
7.42846030289105));
#25046=CARTESIAN_POINT('Ctrl Pts',(0.0296117181373077,1.57084962005681,
7.4270413400413));
#25047=CARTESIAN_POINT('Ctrl Pts',(0.0612630953454002,1.57112724793077,
7.42562339041052));
#25048=CARTESIAN_POINT('Ctrl Pts',(0.0929408476792332,1.57046939552494,
7.42420577971289));
#25049=CARTESIAN_POINT('Ctrl Pts',(0.105200379607973,1.57021480162293,7.42365715355322));
#25050=CARTESIAN_POINT('Ctrl Pts',(0.117460267523568,1.56982005993498,7.42310873898429));
#25051=CARTESIAN_POINT('Ctrl Pts',(0.129708286104984,1.56928654809906,7.42256093565192));
#25052=CARTESIAN_POINT('Ctrl Pts',(0.192428535028528,1.56655451475585,7.41975571771902));
#25053=CARTESIAN_POINT('Ctrl Pts',(0.254912080108278,1.56018641116159,7.41696316059146));
#25054=CARTESIAN_POINT('Ctrl Pts',(0.316835955987319,1.55031158486179,7.41417821827426));
#25055=CARTESIAN_POINT('Ctrl Pts',(0.379261168612821,1.54035681180124,7.41137072901695));
#25056=CARTESIAN_POINT('Ctrl Pts',(0.441118681165113,1.52683817797346,7.40857097836836));
#25057=CARTESIAN_POINT('Ctrl Pts',(0.502077268456636,1.50983552777742,7.40577379678119));
#25058=CARTESIAN_POINT('Ctrl Pts',(0.518104654250298,1.50536514802758,7.40503835473071));
#25059=CARTESIAN_POINT('Ctrl Pts',(0.534069848209942,1.50065364953946,7.40430309027496));
#25060=CARTESIAN_POINT('Ctrl Pts',(0.549966680795085,1.49570190223715,7.40356790945547));
#25061=CARTESIAN_POINT('Ctrl Pts',(0.559908491182372,1.4926051008774,7.40310813054867));
#25062=CARTESIAN_POINT('Ctrl Pts',(0.569821116728089,1.48941503409471,7.4026484967243));
#25063=CARTESIAN_POINT('Ctrl Pts',(0.579694961183896,1.486134869268,7.40218936420725));
#25064=CARTESIAN_POINT('Ctrl Pts',(0.640449229714658,1.46595184779153,7.39936429841276));
#25065=CARTESIAN_POINT('Ctrl Pts',(0.69982505895545,1.44233435228215,7.39655407027566));
#25066=CARTESIAN_POINT('Ctrl Pts',(0.757493396577592,1.41540064986381,7.39375356846506));
#25067=CARTESIAN_POINT('Ctrl Pts',(0.814802366573082,1.38863478825924,7.39097051833992));
#25068=CARTESIAN_POINT('Ctrl Pts',(0.870426121162267,1.35859365369072,7.38819707369729));
#25069=CARTESIAN_POINT('Ctrl Pts',(0.924030095744784,1.32534364884642,7.38542821816778));
#25070=CARTESIAN_POINT('Ctrl Pts',(0.960999915716867,1.30241164235365,7.38351858196539));
#25071=CARTESIAN_POINT('Ctrl Pts',(0.997008764456124,1.27795226352036,7.38161112864094));
#25072=CARTESIAN_POINT('Ctrl Pts',(1.03193962221215,1.25197434532887,7.3797042125328));
#25073=CARTESIAN_POINT('Ctrl Pts',(1.0531065792895,1.23623257674251,7.37854868375383));
#25074=CARTESIAN_POINT('Ctrl Pts',(1.07387756970412,1.21993300461795,7.37739335223873));
#25075=CARTESIAN_POINT('Ctrl Pts',(1.09422502955045,1.2030757852037,7.37623785181303));
#25076=CARTESIAN_POINT('Ctrl Pts',(1.10258166584356,1.19615257942657,7.37576329150589));
#25077=CARTESIAN_POINT('Ctrl Pts',(1.11086633597203,1.18913559341204,7.3752887282991));
#25078=CARTESIAN_POINT('Ctrl Pts',(1.11906690491304,1.18203401934788,7.37481473623418));
#25079=CARTESIAN_POINT('Ctrl Pts',(1.12385025457867,1.17789170773882,7.37453825910173));
#25080=CARTESIAN_POINT('Ctrl Pts',(1.12860592464056,1.17371985114455,7.37426192347451));
#25081=CARTESIAN_POINT('Ctrl Pts',(1.13333360310225,1.16951854601392,7.37398572456616));
#25082=CARTESIAN_POINT('Ctrl Pts',(1.17895537492945,1.12897624060986,7.37132042410681));
#25083=CARTESIAN_POINT('Ctrl Pts',(1.22197272212526,1.08569548753383,7.36866785506909));
#25084=CARTESIAN_POINT('Ctrl Pts',(1.2623504524016,1.0400250384405,7.36602371637222));
#25085=CARTESIAN_POINT('Ctrl Pts',(1.30450707484485,0.992342519733652,7.36326308678831));
#25086=CARTESIAN_POINT('Ctrl Pts',(1.34378698003833,0.942054513171778,7.36051164672689));
#25087=CARTESIAN_POINT('Ctrl Pts',(1.38011608577908,0.889512321374444,7.35776450122604));
#25088=CARTESIAN_POINT('Ctrl Pts',(1.41047885103542,0.845599150293909,7.35546852029652));
#25089=CARTESIAN_POINT('Ctrl Pts',(1.43877996472123,0.800110306074669,7.35317553916464));
#25090=CARTESIAN_POINT('Ctrl Pts',(1.46495451960825,0.753233209535809,7.35088270017959));
#25091=CARTESIAN_POINT('Ctrl Pts',(1.47224608288955,0.740174446270043,7.35024397372845));
#25092=CARTESIAN_POINT('Ctrl Pts',(1.47937249019278,0.727007875170104,7.34960525830843));
#25093=CARTESIAN_POINT('Ctrl Pts',(1.48633203561836,0.713737394565328,7.34896649214163));
#25094=CARTESIAN_POINT('Ctrl Pts',(1.49231636613785,0.702326456460141,7.34841723387359));
#25095=CARTESIAN_POINT('Ctrl Pts',(1.49817791288619,0.690837217360077,7.34786787112171));
#25096=CARTESIAN_POINT('Ctrl Pts',(1.50390644072503,0.679291229674037,7.3473192635151));
#25097=CARTESIAN_POINT('Ctrl Pts',(1.53283760232342,0.620979767295612,7.34454859437159));
#25098=CARTESIAN_POINT('Ctrl Pts',(1.55843652026989,0.561117048195595,7.34179201389979));
#25099=CARTESIAN_POINT('Ctrl Pts',(1.58063784893836,0.500065381838401,7.33904470742869));
#25100=CARTESIAN_POINT('Ctrl Pts',(1.6031119912636,0.438263502347606,7.3362636415941));
#25101=CARTESIAN_POINT('Ctrl Pts',(1.62210502961578,0.375242296860671,7.33349207908152));
#25102=CARTESIAN_POINT('Ctrl Pts',(1.63750518239391,0.311348169568812,7.33072502553951));
#25103=CARTESIAN_POINT('Ctrl Pts',(1.65022992907376,0.258554109936303,7.32843868098962));
#25104=CARTESIAN_POINT('Ctrl Pts',(1.66050103147123,0.20516326683894,7.32615541484386));
#25105=CARTESIAN_POINT('Ctrl Pts',(1.66822949082188,0.151363515297575,7.32387240968315));
#25106=CARTESIAN_POINT('Ctrl Pts',(1.67108031331177,0.13151822211743,7.32303026998087));
#25107=CARTESIAN_POINT('Ctrl Pts',(1.67358492004799,0.111617257557933,7.32218816579018));
#25108=CARTESIAN_POINT('Ctrl Pts',(1.67573795844748,0.091670001678837,7.32134595570008));
#25109=CARTESIAN_POINT('Ctrl Pts',(1.67695445834914,0.0803994944639542,
7.32087009400991));
#25110=CARTESIAN_POINT('Ctrl Pts',(1.67805865914088,0.0691137533863127,
7.3203941797156));
#25111=CARTESIAN_POINT('Ctrl Pts',(1.67904845798992,0.0578298683786967,
7.31991883455417));
#25112=CARTESIAN_POINT('Ctrl Pts',(1.68482856592515,-0.00806440229655341,
7.31714297121365));
#25113=CARTESIAN_POINT('Ctrl Pts',(1.68672581172374,-0.0740201346390124,
7.31438118276366));
#25114=CARTESIAN_POINT('Ctrl Pts',(1.68463949062778,-0.139690992105407,
7.31162863136205));
#25115=CARTESIAN_POINT('Ctrl Pts',(1.68257287237932,-0.204741665606402,
7.30890207456915));
#25116=CARTESIAN_POINT('Ctrl Pts',(1.67659788793627,-0.2695138491763,7.30618458118234));
#25117=CARTESIAN_POINT('Ctrl Pts',(1.6665669476348,-0.3336793478161,7.30347144913232));
#25118=CARTESIAN_POINT('Ctrl Pts',(1.65656393293128,-0.397666213161047,
7.30076587029591));
#25119=CARTESIAN_POINT('Ctrl Pts',(1.64252742158424,-0.461050667219861,
7.29806462854663));
#25120=CARTESIAN_POINT('Ctrl Pts',(1.62468485220914,-0.523589263699737,
7.29536306097687));
#25121=CARTESIAN_POINT('Ctrl Pts',(1.62063291677799,-0.537791386138751,
7.29474955195105));
#25122=CARTESIAN_POINT('Ctrl Pts',(1.61638449230085,-0.551949831001097,
7.29413602612215));
#25123=CARTESIAN_POINT('Ctrl Pts',(1.61194189299792,-0.566061632343824,
7.29352242888019));
#25124=CARTESIAN_POINT('Ctrl Pts',(1.60819661792182,-0.577958401384625,
7.29300514377289));
#25125=CARTESIAN_POINT('Ctrl Pts',(1.60431575784587,-0.589814146380397,
7.2924881495291));
#25126=CARTESIAN_POINT('Ctrl Pts',(1.60030378247776,-0.601620053553602,
7.29197172819479));
#25127=CARTESIAN_POINT('Ctrl Pts',(1.57922949506156,-0.663634661857349,
7.28925904662807));
#25128=CARTESIAN_POINT('Ctrl Pts',(1.55452233752644,-0.724336859414935,
7.28655946062951));
#25129=CARTESIAN_POINT('Ctrl Pts',(1.52646885207918,-0.783492431203164,
7.28386844992972));
#25130=CARTESIAN_POINT('Ctrl Pts',(1.49785765329009,-0.843824036953083,
7.28112394097306));
#25131=CARTESIAN_POINT('Ctrl Pts',(1.46576530908513,-0.902547787676455,
7.27838835166439));
#25132=CARTESIAN_POINT('Ctrl Pts',(1.43044176155356,-0.95940342094092,7.27565688674544));
#25133=CARTESIAN_POINT('Ctrl Pts',(1.40719192683218,-0.996825598744453,
7.27385904614475));
#25134=CARTESIAN_POINT('Ctrl Pts',(1.38254116404519,-1.03343820105651,7.27206299232293));
#25135=CARTESIAN_POINT('Ctrl Pts',(1.35654982896749,-1.06916144614065,7.2702673579332));
#25136=CARTESIAN_POINT('Ctrl Pts',(1.34005703462379,-1.09182962123443,7.26912793863759));
#25137=CARTESIAN_POINT('Ctrl Pts',(1.32302428798857,-1.11413959500617,7.26798868822771));
#25138=CARTESIAN_POINT('Ctrl Pts',(1.30546545072429,-1.13606969941564,7.26684925734159));
#25139=CARTESIAN_POINT('Ctrl Pts',(1.29557863985671,-1.1484178288128,7.26620768082384));
#25140=CARTESIAN_POINT('Ctrl Pts',(1.28552143085819,-1.16064953781435,7.26556582874875));
#25141=CARTESIAN_POINT('Ctrl Pts',(1.27531693894013,-1.17273679271259,7.26492492457875));
#25142=CARTESIAN_POINT('Ctrl Pts',(1.23124484751569,-1.2249403328029,7.26215692913113));
#25143=CARTESIAN_POINT('Ctrl Pts',(1.18437118678711,-1.27452793646465,7.25940270292496));
#25144=CARTESIAN_POINT('Ctrl Pts',(1.1349613540182,-1.32123869434595,7.25665745327404));
#25145=CARTESIAN_POINT('Ctrl Pts',(1.0857776821155,-1.36773564568569,7.25392476930092));
#25146=CARTESIAN_POINT('Ctrl Pts',(1.03408031096501,-1.41138288844598,7.25120097989535));
#25147=CARTESIAN_POINT('Ctrl Pts',(0.980088635865932,-1.45189422149834,
7.24848135788222));
#25148=CARTESIAN_POINT('Ctrl Pts',(0.928612197667789,-1.49051830805181,
7.24588843120928));
#25149=CARTESIAN_POINT('Ctrl Pts',(0.875049469874555,-1.52629233307795,
7.24329929269164));
#25150=CARTESIAN_POINT('Ctrl Pts',(0.819562927233232,-1.55893273310611,
7.24070984551053));
#25151=CARTESIAN_POINT('Ctrl Pts',(0.806531597661789,-1.56659851637287,
7.24010169913812));
#25152=CARTESIAN_POINT('Ctrl Pts',(0.793394057897985,-1.57409127964972,
7.2394935357407));
#25153=CARTESIAN_POINT('Ctrl Pts',(0.78015224431478,-1.58140700410033,7.23888530224817));
#25154=CARTESIAN_POINT('Ctrl Pts',(0.770009447983695,-1.58701060987914,
7.23841941527599));
#25155=CARTESIAN_POINT('Ctrl Pts',(0.759805087672894,-1.59251043302504,
7.23795347189941));
#25156=CARTESIAN_POINT('Ctrl Pts',(0.749553755678445,-1.59789772385032,
7.23748806565584));
#25157=CARTESIAN_POINT('Ctrl Pts',(0.716202490399591,-1.61542451603163,
7.23597393197059));
#25158=CARTESIAN_POINT('Ctrl Pts',(0.682319909404191,-1.63177984026051,
7.23446389597977));
#25159=CARTESIAN_POINT('Ctrl Pts',(0.647945625107734,-1.64691812240344,
7.23295717369848));
#25160=CARTESIAN_POINT('Ctrl Pts',(0.587919642023283,-1.67335329876966,
7.23032606477447));
#25161=CARTESIAN_POINT('Ctrl Pts',(0.52639576498612,-1.69608014520221,7.22770506060276));
#25162=CARTESIAN_POINT('Ctrl Pts',(0.46370862765048,-1.71520377795159,7.22508998649035));
#25163=CARTESIAN_POINT('Ctrl Pts',(0.400150801058184,-1.73459302725791,
7.22243859046197));
#25164=CARTESIAN_POINT('Ctrl Pts',(0.335396320744255,-1.75027834108098,
7.21979329036732));
#25165=CARTESIAN_POINT('Ctrl Pts',(0.269772608446838,-1.76232212244813,
7.21714973513363));
#25166=CARTESIAN_POINT('Ctrl Pts',(0.241062234316718,-1.76759127679625,
7.2159931797189));
#25167=CARTESIAN_POINT('Ctrl Pts',(0.2121852884367,-1.77216281037181,7.21483695828146));
#25168=CARTESIAN_POINT('Ctrl Pts',(0.183168585619119,-1.77603911617646,
7.21368070646147));
#25169=CARTESIAN_POINT('Ctrl Pts',(0.164433789661126,-1.77854187463173,
7.21293416602716));
#25170=CARTESIAN_POINT('Ctrl Pts',(0.145640727943501,-1.78075477785065,
7.21218761292724));
#25171=CARTESIAN_POINT('Ctrl Pts',(0.126796600025785,-1.78267808932064,
7.21144094909238));
#25172=CARTESIAN_POINT('Ctrl Pts',(0.114847127630937,-1.78389770306013,
7.21096747327424));
#25173=CARTESIAN_POINT('Ctrl Pts',(0.102876237812544,-1.78500084411828,
7.21049391856396));
#25174=CARTESIAN_POINT('Ctrl Pts',(0.0909023739078884,-1.78598642534176,
7.21002091434047));
#25175=CARTESIAN_POINT('Ctrl Pts',(0.0223150311249881,-1.79163192104421,
7.20731150465678));
#25176=CARTESIAN_POINT('Ctrl Pts',(-0.0464949765975819,-1.79343822563924,
7.204615131498));
#25177=CARTESIAN_POINT('Ctrl Pts',(-0.115169948787061,-1.79150548386327,
7.201927305065));
#25178=CARTESIAN_POINT('Ctrl Pts',(-0.184810802193317,-1.78954555898233,
7.1992016756161));
#25179=CARTESIAN_POINT('Ctrl Pts',(-0.254313838210283,-1.78374072590431,
7.19648483499498));
#25180=CARTESIAN_POINT('Ctrl Pts',(-0.323317077031426,-1.77414310096439,
7.19377210128489));
#25181=CARTESIAN_POINT('Ctrl Pts',(-0.390207228852162,-1.76483938420678,
7.19114243965136));
#25182=CARTESIAN_POINT('Ctrl Pts',(-0.456628689115353,-1.75197132856033,
7.18851663724823));
#25183=CARTESIAN_POINT('Ctrl Pts',(-0.522247153731527,-1.73553989954365,
7.18589042924469));
#25184=CARTESIAN_POINT('Ctrl Pts',(-0.542667798244601,-1.73042639417967,
7.18507314617701));
#25185=CARTESIAN_POINT('Ctrl Pts',(-0.563010584939934,-1.72496745463069,
7.1842558238281));
#25186=CARTESIAN_POINT('Ctrl Pts',(-0.583265123016525,-1.71916221233715,
7.18343833365983));
#25187=CARTESIAN_POINT('Ctrl Pts',(-0.594324986363522,-1.71599229623144,
7.18299194828612));
#25188=CARTESIAN_POINT('Ctrl Pts',(-0.605348577565269,-1.71272196767285,
7.18254591460309));
#25189=CARTESIAN_POINT('Ctrl Pts',(-0.616333858846904,-1.70935174383982,
7.18210023125036));
#25190=CARTESIAN_POINT('Ctrl Pts',(-0.683725730938223,-1.68867628841438,
7.17936607863924));
#25191=CARTESIAN_POINT('Ctrl Pts',(-0.749681756569652,-1.66424383897131,
7.17664487770965));
#25192=CARTESIAN_POINT('Ctrl Pts',(-0.813838416597903,-1.63611281928401,
7.17393200937892));
#25193=CARTESIAN_POINT('Ctrl Pts',(-0.876849560193779,-1.60848407863208,
7.17126757928126));
#25194=CARTESIAN_POINT('Ctrl Pts',(-0.938126029319885,-1.57728744952324,
7.16861118688198));
#25195=CARTESIAN_POINT('Ctrl Pts',(-0.997312296090875,-1.54253001527406,
7.16595845612799));
#25196=CARTESIAN_POINT('Ctrl Pts',(-1.02347117496609,-1.52716808146505,
7.16478601417029));
#25197=CARTESIAN_POINT('Ctrl Pts',(-1.0492215115725,-1.51110995120918,7.16361428748691));
#25198=CARTESIAN_POINT('Ctrl Pts',(-1.07453112510484,-1.49435330423123,
7.16244289826465));
#25199=CARTESIAN_POINT('Ctrl Pts',(-1.10516814559263,-1.47406955963299,
7.16102494395429));
#25200=CARTESIAN_POINT('Ctrl Pts',(-1.13515946112038,-1.45276234916859,
7.15960748412057));
#25201=CARTESIAN_POINT('Ctrl Pts',(-1.16448435570839,-1.43047866030764,
7.15818984863178));
#25202=CARTESIAN_POINT('Ctrl Pts',(-1.17968931872586,-1.41892456370188,
7.15745480438074));
#25203=CARTESIAN_POINT('Ctrl Pts',(-1.1947150759586,-1.40710789339051,7.15671971290617));
#25204=CARTESIAN_POINT('Ctrl Pts',(-1.20955844125675,-1.39503487170675,
7.15598448079515));
#25205=CARTESIAN_POINT('Ctrl Pts',(-1.2184705964626,-1.38778606788849,7.1555430375945));
#25206=CARTESIAN_POINT('Ctrl Pts',(-1.22730979594949,-1.38045068721632,
7.15510189992037));
#25207=CARTESIAN_POINT('Ctrl Pts',(-1.23607420347025,-1.37303174210186,
7.15466112096385));
#25208=CARTESIAN_POINT('Ctrl Pts',(-1.28876418024182,-1.32843043336258,
7.1520112404185));
#25209=CARTESIAN_POINT('Ctrl Pts',(-1.33877042848354,-1.2807988909053,7.14937346465996));
#25210=CARTESIAN_POINT('Ctrl Pts',(-1.38599825103533,-1.23050256527184,
7.14674359103655));
#25211=CARTESIAN_POINT('Ctrl Pts',(-1.43425343070737,-1.17911213270163,
7.14405650919887));
#25212=CARTESIAN_POINT('Ctrl Pts',(-1.47960859192691,-1.1249390060584,7.14137767702936));
#25213=CARTESIAN_POINT('Ctrl Pts',(-1.52193138288134,-1.06832685423381,
7.13870261160338));
#25214=CARTESIAN_POINT('Ctrl Pts',(-1.55066539724144,-1.02989143098312,
7.13688644195504));
#25215=CARTESIAN_POINT('Ctrl Pts',(-1.57800101601077,-0.990330805152557,
7.13507200854792));
#25216=CARTESIAN_POINT('Ctrl Pts',(-1.60388667803358,-0.949743456777433,
7.13325790847962));
#25217=CARTESIAN_POINT('Ctrl Pts',(-1.62003594041973,-0.924422267854757,
7.13212614766269));
#25218=CARTESIAN_POINT('Ctrl Pts',(-1.63562069179463,-0.898701332888775,
7.13099451658541));
#25219=CARTESIAN_POINT('Ctrl Pts',(-1.65062655993749,-0.872603512387977,
7.12986267459833));
#25220=CARTESIAN_POINT('Ctrl Pts',(-1.65635574489922,-0.862639461036616,
7.12943054151348));
#25221=CARTESIAN_POINT('Ctrl Pts',(-1.66200053139848,-0.852620464599865,
7.12899837768465));
#25222=CARTESIAN_POINT('Ctrl Pts',(-1.66756006049801,-0.842547771324513,
7.12856616415337));
#25223=CARTESIAN_POINT('Ctrl Pts',(-1.67344140782474,-0.831892011347815,
7.12810893156204));
#25224=CARTESIAN_POINT('Ctrl Pts',(-1.67922337730384,-0.821183277061747,
7.1276519494335));
#25225=CARTESIAN_POINT('Ctrl Pts',(-1.68490302697532,-0.810427767612281,
7.1271953846437));
#25226=CARTESIAN_POINT('Ctrl Pts',(-1.71867201689079,-0.746479687863883,
7.12448082781816));
#25227=CARTESIAN_POINT('Ctrl Pts',(-1.74885449180758,-0.680831600304512,
7.12177889893296));
#25228=CARTESIAN_POINT('Ctrl Pts',(-1.77532011389704,-0.613841133314895,
7.11908508207449));
#25229=CARTESIAN_POINT('Ctrl Pts',(-1.80172135822353,-0.547013620983615,
7.11639781793949));
#25230=CARTESIAN_POINT('Ctrl Pts',(-1.82442431805884,-0.478849290745972,
7.11371862641413));
#25231=CARTESIAN_POINT('Ctrl Pts',(-1.84325651205081,-0.409674689769748,
7.11104302445964));
#25232=CARTESIAN_POINT('Ctrl Pts',(-1.86148527154818,-0.34271663033918,
7.10845315603751));
#25233=CARTESIAN_POINT('Ctrl Pts',(-1.87608759212419,-0.274811091848995,
7.10586665083265));
#25234=CARTESIAN_POINT('Ctrl Pts',(-1.88686151657838,-0.206241373327113,
7.1032794430912));
#25235=CARTESIAN_POINT('Ctrl Pts',(-1.8894237591873,-0.189934199908044,
7.10266415625292));
#25236=CARTESIAN_POINT('Ctrl Pts',(-1.89176925852511,-0.173589436851263,
7.10204882968071));
#25237=CARTESIAN_POINT('Ctrl Pts',(-1.89389487850133,-0.157210868172391,
7.10143340868806));
#25238=CARTESIAN_POINT('Ctrl Pts',(-1.89540717923759,-0.145558116622667,
7.10099555919912));
#25239=CARTESIAN_POINT('Ctrl Pts',(-1.89680805540638,-0.133888495556873,
7.10055767143479));
#25240=CARTESIAN_POINT('Ctrl Pts',(-1.89809506960791,-0.12221735851089,
7.10012024866215));
#25241=CARTESIAN_POINT('Ctrl Pts',(-1.90260558085945,-0.0813143172688235,
7.09858724278285));
#25242=CARTESIAN_POINT('Ctrl Pts',(-1.90572389008592,-0.0403491830271802,
7.09705830708501));
#25243=CARTESIAN_POINT('Ctrl Pts',(-1.90742224034152,0.000616434489977578,
7.09553262952215));
#25244=CARTESIAN_POINT('',(0.084982434829279,1.94905960819019,7.046));
#25245=CARTESIAN_POINT('Ctrl Pts',(0.0849160311153282,1.94854955259671,
7.046));
#25246=CARTESIAN_POINT('Ctrl Pts',(0.0133469932817959,1.94202022424704,
7.05556311378236));
#25247=CARTESIAN_POINT('Ctrl Pts',(-0.057643443386169,1.9317481562341,7.06516697216295));
#25248=CARTESIAN_POINT('Ctrl Pts',(-0.127716536696194,1.91775362299336,
7.07483035053949));
#25249=CARTESIAN_POINT('Ctrl Pts',(-0.195999508457667,1.90411660095032,
7.08424686352096));
#25250=CARTESIAN_POINT('Ctrl Pts',(-0.263412231749455,1.88694439734026,
7.09371989428859));
#25251=CARTESIAN_POINT('Ctrl Pts',(-0.329616946053496,1.86621372408347,
7.10326681575032));
#25252=CARTESIAN_POINT('Ctrl Pts',(-0.373950818831073,1.85233146448275,
7.10965989524551));
#25253=CARTESIAN_POINT('Ctrl Pts',(-0.41774246810674,1.83685263442241,7.11608610945697));
#25254=CARTESIAN_POINT('Ctrl Pts',(-0.460881457798893,1.81976080684648,
7.12255067528795));
#25255=CARTESIAN_POINT('Ctrl Pts',(-0.497884301533585,1.80510014303758,
7.12809571287374));
#25256=CARTESIAN_POINT('Ctrl Pts',(-0.53440686918178,1.7892525808674,7.13366896766314));
#25257=CARTESIAN_POINT('Ctrl Pts',(-0.570374125039445,1.77220369526276,
7.13927373202269));
#25258=CARTESIAN_POINT('Ctrl Pts',(-0.580625413497348,1.76734446872319,
7.14087118656344));
#25259=CARTESIAN_POINT('Ctrl Pts',(-0.590829427779041,1.7623885644236,7.14247087519816));
#25260=CARTESIAN_POINT('Ctrl Pts',(-0.600974912742468,1.75734066833771,
7.14407135449713));
#25261=CARTESIAN_POINT('Ctrl Pts',(-0.660532286239387,1.72770783820246,
7.15346670067592));
#25262=CARTESIAN_POINT('Ctrl Pts',(-0.718171394717493,1.69486290257124,
7.16290421661148));
#25263=CARTESIAN_POINT('Ctrl Pts',(-0.77359140837187,1.65879255638639,7.17240215454285));
#25264=CARTESIAN_POINT('Ctrl Pts',(-0.79145555504589,1.64716560228914,7.17546373004814));
#25265=CARTESIAN_POINT('Ctrl Pts',(-0.809088855973432,1.63520322368412,
7.17853158362642));
#25266=CARTESIAN_POINT('Ctrl Pts',(-0.826480388876073,1.62290416848565,
7.18160632658995));
#25267=CARTESIAN_POINT('Ctrl Pts',(-0.88415727734301,1.5821158585131,7.19180333498275));
#25268=CARTESIAN_POINT('Ctrl Pts',(-0.93917932864386,1.5376265413157,7.20207611531283));
#25269=CARTESIAN_POINT('Ctrl Pts',(-0.99133911172057,1.48977648468554,7.21244696501856));
#25270=CARTESIAN_POINT('Ctrl Pts',(-1.03697892191269,1.44790768513415,7.22152145851107));
#25271=CARTESIAN_POINT('Ctrl Pts',(-1.0804266997828,1.40346470822021,7.2306710363693));
#25272=CARTESIAN_POINT('Ctrl Pts',(-1.12150612234599,1.35666626833897,7.23991063613496));
#25273=CARTESIAN_POINT('Ctrl Pts',(-1.12930267296081,1.34778429331443,7.24166423934404));
#25274=CARTESIAN_POINT('Ctrl Pts',(-1.13701438607344,1.338816634524,7.24342123717376));
#25275=CARTESIAN_POINT('Ctrl Pts',(-1.14462934985433,1.32977774514085,7.24517924126443));
#25276=CARTESIAN_POINT('Ctrl Pts',(-1.18689780114357,1.27960549657953,7.25493741115345));
#25277=CARTESIAN_POINT('Ctrl Pts',(-1.22626964349749,1.22715044372182,7.26474446593405));
#25278=CARTESIAN_POINT('Ctrl Pts',(-1.2626041554744,1.17270468062558,7.27462138727731));
#25279=CARTESIAN_POINT('Ctrl Pts',(-1.29870272792618,1.11861246314731,7.28443417245898));
#25280=CARTESIAN_POINT('Ctrl Pts',(-1.33180351900955,1.06255418531111,7.29431591978697));
#25281=CARTESIAN_POINT('Ctrl Pts',(-1.36171904589852,1.00480435475497,7.30428720484495));
#25282=CARTESIAN_POINT('Ctrl Pts',(-1.39100085763464,0.948277866941019,
7.31404726332289));
#25283=CARTESIAN_POINT('Ctrl Pts',(-1.41723097430462,0.890129769006774,
7.32389310626744));
#25284=CARTESIAN_POINT('Ctrl Pts',(-1.44018415693848,0.83062133555421,7.33384402917814));
#25285=CARTESIAN_POINT('Ctrl Pts',(-1.44632047771148,0.814712307068312,
7.33650431624776));
#25286=CARTESIAN_POINT('Ctrl Pts',(-1.45222231211246,0.798706119319694,
7.33917211349499));
#25287=CARTESIAN_POINT('Ctrl Pts',(-1.45788473508532,0.78260794455952,7.34184778960142));
#25288=CARTESIAN_POINT('Ctrl Pts',(-1.46140114941093,0.772610836852428,
7.34350940792919));
#25289=CARTESIAN_POINT('Ctrl Pts',(-1.4648248277114,0.762579164108622,7.34517391187186));
#25290=CARTESIAN_POINT('Ctrl Pts',(-1.46815093425694,0.752525994362274,
7.34683944075502));
#25291=CARTESIAN_POINT('Ctrl Pts',(-1.4875809575628,0.693798674658319,7.35656891411169));
#25292=CARTESIAN_POINT('Ctrl Pts',(-1.50372373374688,0.634230525264841,
7.36635120065226));
#25293=CARTESIAN_POINT('Ctrl Pts',(-1.51642546703182,0.574066612526935,
7.37620769393241));
#25294=CARTESIAN_POINT('Ctrl Pts',(-1.52890893161854,0.514936566476241,
7.385894811592));
#25295=CARTESIAN_POINT('Ctrl Pts',(-1.53806859003218,0.455230176794947,
7.39565360754218));
#25296=CARTESIAN_POINT('Ctrl Pts',(-1.54370934814325,0.395188284726392,
7.40550439129109));
#25297=CARTESIAN_POINT('Ctrl Pts',(-1.54918565956382,0.33689681170573,7.41506799222619));
#25298=CARTESIAN_POINT('Ctrl Pts',(-1.55134510253712,0.278288450517533,
7.42471829564676));
#25299=CARTESIAN_POINT('Ctrl Pts',(-1.54996382900015,0.219602494440036,
7.43447388607445));
#25300=CARTESIAN_POINT('Ctrl Pts',(-1.54949240817649,0.199573310494113,
7.43780341375428));
#25301=CARTESIAN_POINT('Ctrl Pts',(-1.5486081708139,0.179535297751125,7.44114520545616));
#25302=CARTESIAN_POINT('Ctrl Pts',(-1.54730100999696,0.159498697368912,
7.4445));
#25303=CARTESIAN_POINT('',(-1.49051052577446,1.26051379553366,7.046));
#25304=CARTESIAN_POINT('Origin',(0.,0.,7.046));
#25305=CARTESIAN_POINT('Ctrl Pts',(-1.90742224034152,0.000616434489977578,
7.09553262952215));
#25306=CARTESIAN_POINT('Ctrl Pts',(-1.90876164805009,0.0329240599094907,
7.09432940051696));
#25307=CARTESIAN_POINT('Ctrl Pts',(-1.90921779267002,0.0652320529994964,
7.09312819770054));
#25308=CARTESIAN_POINT('Ctrl Pts',(-1.90877477964874,0.0975109530601205,
7.09192862283081));
#25309=CARTESIAN_POINT('Ctrl Pts',(-1.90781024899833,0.16778877103618,7.08931690111213));
#25310=CARTESIAN_POINT('Ctrl Pts',(-1.90258719753853,0.237928585345474,
7.08671289622934));
#25311=CARTESIAN_POINT('Ctrl Pts',(-1.89333689480301,0.307653748465392,
7.08411249814515));
#25312=CARTESIAN_POINT('Ctrl Pts',(-1.88389965579861,0.378787964046921,
7.0814595494873));
#25313=CARTESIAN_POINT('Ctrl Pts',(-1.87027048866354,0.449491484193812,
7.0788103548782));
#25314=CARTESIAN_POINT('Ctrl Pts',(-1.8526408196263,0.519466411196971,7.0761605500361));
#25315=CARTESIAN_POINT('Ctrl Pts',(-1.84839799409914,0.536306852496432,
7.07552283757523));
#25316=CARTESIAN_POINT('Ctrl Pts',(-1.8439232315986,0.553105040705889,7.07488508977019));
#25317=CARTESIAN_POINT('Ctrl Pts',(-1.83921877202327,0.569856697426902,
7.07424724578707));
#25318=CARTESIAN_POINT('Ctrl Pts',(-1.83514299244073,0.584369748149054,
7.07369464002192));
#25319=CARTESIAN_POINT('Ctrl Pts',(-1.83089368872409,0.598851100707912,
7.07314183740804));
#25320=CARTESIAN_POINT('Ctrl Pts',(-1.82648012174354,0.613273349358239,
7.07258974257699));
#25321=CARTESIAN_POINT('Ctrl Pts',(-1.80525925753629,0.682616939592868,
7.06993521631944));
#25322=CARTESIAN_POINT('Ctrl Pts',(-1.78021580797096,0.750706522102631,
7.06729279368472));
#25323=CARTESIAN_POINT('Ctrl Pts',(-1.75159954554489,0.817253861437449,
7.06465826007958));
#25324=CARTESIAN_POINT('Ctrl Pts',(-1.72257788914062,0.884743947600279,
7.06198640419794));
#25325=CARTESIAN_POINT('Ctrl Pts',(-1.68988110151814,0.950648721336099,
7.05932266244995));
#25326=CARTESIAN_POINT('Ctrl Pts',(-1.65371662519363,1.01465825897231,7.05666263857406));
#25327=CARTESIAN_POINT('Ctrl Pts',(-1.61767133058481,1.07845685019671,7.05401138093072));
#25328=CARTESIAN_POINT('Ctrl Pts',(-1.57818065931587,1.14037360389397,7.051363816695));
#25329=CARTESIAN_POINT('Ctrl Pts',(-1.53540446982221,1.20007853919048,7.04871559292653));
#25330=CARTESIAN_POINT('Ctrl Pts',(-1.52078518671176,1.2204834271088,7.04781053023934));
#25331=CARTESIAN_POINT('Ctrl Pts',(-1.50578179227618,1.24062970905854,7.04690539051781));
#25332=CARTESIAN_POINT('Ctrl Pts',(-1.49039960333531,1.26050328917698,7.046));
#25333=CARTESIAN_POINT('',(-1.,-1.22464679914735E-16,8.));
#25334=CARTESIAN_POINT('',(-1.5,-1.83697019872103E-16,7.5));
#25335=CARTESIAN_POINT('Origin',(0.,0.,8.));
#25336=CARTESIAN_POINT('Ctrl Pts',(1.13509973994373,-1.59049193030951,-0.230074082272067));
#25337=CARTESIAN_POINT('Ctrl Pts',(1.66385265555159,-1.21313239420412,-0.193036768839232));
#25338=CARTESIAN_POINT('Ctrl Pts',(2.30633309595034,0.10379526882931,-0.11896214197356));
#25339=CARTESIAN_POINT('Ctrl Pts',(1.1618831159781,1.99754257541113,-0.00785020167505245));
#25340=CARTESIAN_POINT('Ctrl Pts',(-1.04657265959996,2.05782619857144,0.103261738623455));
#25341=CARTESIAN_POINT('Ctrl Pts',(-2.29698513032901,0.238308494988224,
0.214373678921962));
#25342=CARTESIAN_POINT('Ctrl Pts',(-1.44610949780919,-1.80077244555215,
0.32548561922047));
#25343=CARTESIAN_POINT('Ctrl Pts',(0.727982080133343,-2.19148935509534,
0.436597559518978));
#25344=CARTESIAN_POINT('Ctrl Pts',(2.23595404085407,-0.577589325353924,
0.547709499817485));
#25345=CARTESIAN_POINT('Ctrl Pts',(1.69824597043106,1.56497940407905,0.658821440115993));
#25346=CARTESIAN_POINT('Ctrl Pts',(-0.393241729595879,2.27560136836119,
0.7699333804145));
#25347=CARTESIAN_POINT('Ctrl Pts',(-2.12493397204,0.90429099396703,0.881045320713008));
#25348=CARTESIAN_POINT('Ctrl Pts',(-1.91248731439823,-1.29440519809075,
0.992157261011514));
#25349=CARTESIAN_POINT('Ctrl Pts',(0.0497351526023427,-2.30880745912378,
1.10326920131002));
#25350=CARTESIAN_POINT('Ctrl Pts',(1.96645238083605,-1.21084445058012,1.21438114160853));
#25351=CARTESIAN_POINT('Ctrl Pts',(2.0840238587571,0.994948952062592,1.32549308190704));
#25352=CARTESIAN_POINT('Ctrl Pts',(0.294879848465431,2.29044125875909,1.43660502220554));
#25353=CARTESIAN_POINT('Ctrl Pts',(-1.76405540105404,1.49036437523231,1.54771696250405));
#25354=CARTESIAN_POINT('Ctrl Pts',(-2.20902124244616,-0.673277315499274,
1.65882890280256));
#25355=CARTESIAN_POINT('Ctrl Pts',(-0.63290935858251,-2.22092378987733,
1.76994084310107));
#25356=CARTESIAN_POINT('Ctrl Pts',(1.5222639082646,-1.73660290660664,1.88105278339957));
#25357=CARTESIAN_POINT('Ctrl Pts',(2.28468753295219,0.336570763856544,1.99216472369808));
#25358=CARTESIAN_POINT('Ctrl Pts',(0.956804884638204,2.10180906822536,2.10327666399659));
#25359=CARTESIAN_POINT('Ctrl Pts',(-1.24647766157407,1.94406029583798,2.2143886042951));
#25360=CARTESIAN_POINT('Ctrl Pts',(-2.30933289737607,0.00765190922063762,
2.3255005445936));
#25361=CARTESIAN_POINT('Ctrl Pts',(-1.25933333160116,-1.9357573546638,2.43661248489211));
#25362=CARTESIAN_POINT('Ctrl Pts',(0.942855455692524,-2.10810354889204,
2.54772442519062));
#25363=CARTESIAN_POINT('Ctrl Pts',(2.28240695194457,-0.35170369161106,2.65883636548913));
#25364=CARTESIAN_POINT('Ctrl Pts',(1.53373873309094,1.72647689788489,2.76994830578763));
#25365=CARTESIAN_POINT('Ctrl Pts',(-0.618177691355928,2.22506928503553,
2.88106024608615));
#25366=CARTESIAN_POINT('Ctrl Pts',(-2.20451099698397,0.687901333838673,
2.99217218638465));
#25367=CARTESIAN_POINT('Ctrl Pts',(-1.77389315295183,-1.47864128941955,
3.10328412668316));
#25368=CARTESIAN_POINT('Ctrl Pts',(0.279694972942425,-2.29234545893725,
3.21439606698166));
#25369=CARTESIAN_POINT('Ctrl Pts',(2.07738458076118,-1.00873697491097,3.32550800728017));
#25370=CARTESIAN_POINT('Ctrl Pts',(1.97443353669272,1.1977851185115,3.43661994757868));
#25371=CARTESIAN_POINT('Ctrl Pts',(0.0650338075591902,2.30842967941821,
3.54773188787719));
#25372=CARTESIAN_POINT('Ctrl Pts',(-1.90386665125239,1.30704581219857,3.65884382817569));
#25373=CARTESIAN_POINT('Ctrl Pts',(-2.13088147818969,-0.890180378860142,
3.7699557684742));
#25374=CARTESIAN_POINT('Ctrl Pts',(-0.408310273068383,-2.2729627585538,
3.88106770877271));
#25375=CARTESIAN_POINT('Ctrl Pts',(1.6878321574451,-1.57616610457607,3.99217964907122));
#25376=CARTESIAN_POINT('Ctrl Pts',(2.23974323019256,0.562696404915903,4.10329158936972));
#25377=CARTESIAN_POINT('Ctrl Pts',(0.742468479097436,2.18673673263618,4.21440352966824));
#25378=CARTESIAN_POINT('Ctrl Pts',(-1.43410551503643,1.81008794060395,4.32551546996673));
#25379=CARTESIAN_POINT('Ctrl Pts',(-2.29858772583325,-0.222646468261011,
4.43662741026525));
#25380=CARTESIAN_POINT('Ctrl Pts',(-1.06004610686433,-2.05167717429874,
4.54773935056375));
#25381=CARTESIAN_POINT('Ctrl Pts',(1.14835286831205,-2.00358745066383,4.65885129086226));
#25382=CARTESIAN_POINT('Ctrl Pts',(2.30610086989477,-0.122375538925838,
4.76996323116077));
#25383=CARTESIAN_POINT('Ctrl Pts',(1.35395110677505,1.87080018895779,4.88107517145928));
#25384=CARTESIAN_POINT('Ctrl Pts',(-0.836955550366062,2.15234346911026,
4.99218711175778));
#25385=CARTESIAN_POINT('Ctrl Pts',(-2.26211489466594,0.464664680140549,
5.10329905205629));
#25386=CARTESIAN_POINT('Ctrl Pts',(-1.61762005706343,-1.64814504446985,
5.2144109923548));
#25387=CARTESIAN_POINT('Ctrl Pts',(0.506867541264277,-2.25303406293758,
5.3255229326533));
#25388=CARTESIAN_POINT('Ctrl Pts',(2.16761217480869,-0.796576982199858,
5.43663487295182));
#25389=CARTESIAN_POINT('Ctrl Pts',(1.84516460593919,1.38868385957575,5.54774681325032));
#25390=CARTESIAN_POINT('Ctrl Pts',(-0.165459925935554,2.30341092165264,
5.65885875354883));
#25391=CARTESIAN_POINT('Ctrl Pts',(-2.02470376163623,1.11069974665188,5.76997069384733));
#25392=CARTESIAN_POINT('Ctrl Pts',(-2.03150206860296,-1.09820982237999,
5.88108263414585));
#25393=CARTESIAN_POINT('Ctrl Pts',(-0.179645428808579,-2.30235098638037,
5.99219457444435));
#25394=CARTESIAN_POINT('Ctrl Pts',(1.83658550522895,-1.40001438181273,6.10330651474285));
#25395=CARTESIAN_POINT('Ctrl Pts',(2.17246271157681,0.783202663677277,6.21441845504137));
#25396=CARTESIAN_POINT('Ctrl Pts',(0.520757933621259,2.24989134978725,6.32553039533987));
#25397=CARTESIAN_POINT('Ctrl Pts',(-1.60748926038381,1.65803443249082,6.43664233563838));
#25398=CARTESIAN_POINT('Ctrl Pts',(-2.26483986170582,-0.450648314453544,
6.54775427593688));
#25399=CARTESIAN_POINT('Ctrl Pts',(-0.850371985170964,-2.14729633892256,
6.6588662162354));
#25400=CARTESIAN_POINT('Ctrl Pts',(1.34274482878903,-1.87882089420371,6.7699781565339));
#25401=CARTESIAN_POINT('Ctrl Pts',(2.30616083080651,0.107634649639171,6.88109009683241));
#25402=CARTESIAN_POINT('Ctrl Pts',(1.16193045799902,1.99751503787814,6.99220203713092));
#25403=CARTESIAN_POINT('Ctrl Pts',(-1.04999517826429,2.05607780322851,7.10331397742942));
#25404=CARTESIAN_POINT('Ctrl Pts',(-1.87709151778098,0.84653605896511,7.1773886042951));
#25405=CARTESIAN_POINT('Ctrl Pts',(-1.94370052943366,0.200360305148756,
7.21442591772793));
#25406=CARTESIAN_POINT('Ctrl Pts',(1.05793541951256,-1.48236995244729,-0.153382721514712));
#25407=CARTESIAN_POINT('Ctrl Pts',(1.55074360006928,-1.13066339742992,-0.116345408081876));
#25408=CARTESIAN_POINT('Ctrl Pts',(2.14954808422461,0.0967392444982914,
-0.0422707812162042));
#25409=CARTESIAN_POINT('Ctrl Pts',(1.08289805597856,1.8617492085907,0.0688411590823027));
#25410=CARTESIAN_POINT('Ctrl Pts',(-0.975426428816855,1.91793473829667,
0.179953099380811));
#25411=CARTESIAN_POINT('Ctrl Pts',(-2.14083559528361,0.222108233089066,
0.291065039679317));
#25412=CARTESIAN_POINT('Ctrl Pts',(-1.34780266824982,-1.6783555537827,0.402176979977826));
#25413=CARTESIAN_POINT('Ctrl Pts',(0.678493704334455,-2.04251144516605,
0.513288920276332));
#25414=CARTESIAN_POINT('Ctrl Pts',(2.08395341218121,-0.538324680837788,
0.624400860574841));
#25415=CARTESIAN_POINT('Ctrl Pts',(1.58279885012795,1.4585917731467,0.735512800873347));
#25416=CARTESIAN_POINT('Ctrl Pts',(-0.366509073634787,2.12090550597771,
0.846624741171857));
#25417=CARTESIAN_POINT('Ctrl Pts',(-1.9804805111294,0.842817100910752,0.957736681470361));
#25418=CARTESIAN_POINT('Ctrl Pts',(-1.78247602221336,-1.20641125891655,
1.06884862176887));
#25419=CARTESIAN_POINT('Ctrl Pts',(0.0463541464078725,-2.15185423966612,
1.17996056206738));
#25420=CARTESIAN_POINT('Ctrl Pts',(1.83277253201941,-1.12853098869745,1.29107250236589));
#25421=CARTESIAN_POINT('Ctrl Pts',(1.94235147600127,0.927312111837943,1.40218444266439));
#25422=CARTESIAN_POINT('Ctrl Pts',(0.274833853990247,2.13473657748725,1.5132963829629));
#25423=CARTESIAN_POINT('Ctrl Pts',(-1.6441345417364,1.38904908974441,1.62440832326141));
#25424=CARTESIAN_POINT('Ctrl Pts',(-2.05885151110621,-0.627507781172011,
1.73552026355991));
#25425=CARTESIAN_POINT('Ctrl Pts',(-0.589884046505544,-2.06994492084524,
1.84663220385842));
#25426=CARTESIAN_POINT('Ctrl Pts',(1.4187800857734,-1.6185482736686,1.95774414415693));
#25427=CARTESIAN_POINT('Ctrl Pts',(2.12937399117781,0.313690612134129,2.06885608445544));
#25428=CARTESIAN_POINT('Ctrl Pts',(0.891761086185737,1.95892764316774,2.17996802475395));
#25429=CARTESIAN_POINT('Ctrl Pts',(-1.16174184647048,1.81190266569614,2.29107996505245));
#25430=CARTESIAN_POINT('Ctrl Pts',(-2.15234395851487,0.00713173081318942,
2.40219190535096));
#25431=CARTESIAN_POINT('Ctrl Pts',(-1.17372358532974,-1.80416416021932,
2.51330384564946));
#25432=CARTESIAN_POINT('Ctrl Pts',(0.878759942370547,-1.96479422370721,
2.62441578594798));
#25433=CARTESIAN_POINT('Ctrl Pts',(2.1272484445495,-0.327794800258781,2.73552772624649));
#25434=CARTESIAN_POINT('Ctrl Pts',(1.42947484958074,1.60911063316174,2.84663966654499));
#25435=CARTESIAN_POINT('Ctrl Pts',(-0.576153841133258,2.07380860436568,
2.9577516068435));
#25436=CARTESIAN_POINT('Ctrl Pts',(-2.0546478730846,0.641137655651238,3.068863547142));
#25437=CARTESIAN_POINT('Ctrl Pts',(-1.65330352117917,-1.37812294178502,
3.17997548744051));
#25438=CARTESIAN_POINT('Ctrl Pts',(0.260681249517398,-2.1365113297345,3.29108742773902));
#25439=CARTESIAN_POINT('Ctrl Pts',(1.93616353752793,-0.940162821976462,
3.40219936803753));
#25440=CARTESIAN_POINT('Ctrl Pts',(1.84021112721267,1.11635943278533,3.51331130833604));
#25441=CARTESIAN_POINT('Ctrl Pts',(0.0606127955645832,2.15150214150485,
3.62442324863454));
#25442=CARTESIAN_POINT('Ctrl Pts',(-1.77444139357172,1.21819256140342,3.73553518893305));
#25443=CARTESIAN_POINT('Ctrl Pts',(-1.98602370455295,-0.829665728403687,
3.84664712923155));
#25444=CARTESIAN_POINT('Ctrl Pts',(-0.380553254334539,-2.11844626942319,
3.95775906953007));
#25445=CARTESIAN_POINT('Ctrl Pts',(1.57309297035165,-1.46901799937757,4.06887100982856));
#25446=CARTESIAN_POINT('Ctrl Pts',(2.08748501162692,0.524444184281487,4.17998295012709));
#25447=CARTESIAN_POINT('Ctrl Pts',(0.691995314832617,2.038081906987,4.29109489042558));
#25448=CARTESIAN_POINT('Ctrl Pts',(-1.33661471876519,1.68703777951035,4.4022068307241));
#25449=CARTESIAN_POINT('Ctrl Pts',(-2.14232924600648,-0.207510914251802,
4.5133187710226));
#25450=CARTESIAN_POINT('Ctrl Pts',(-0.987983948286119,-1.91220372599474,
4.62443071132112));
#25451=CARTESIAN_POINT('Ctrl Pts',(1.07028759741094,-1.86738315194504,4.73554265161961));
#25452=CARTESIAN_POINT('Ctrl Pts',(2.14933164494543,-0.114056423903322,
4.84665459191812));
#25453=CARTESIAN_POINT('Ctrl Pts',(1.26190922413262,1.74362279637852,4.95776653221663));
#25454=CARTESIAN_POINT('Ctrl Pts',(-0.780059135009386,2.00602670479084,
5.06887847251514));
#25455=CARTESIAN_POINT('Ctrl Pts',(-2.10833584561709,0.433076676893185,
5.17999041281365));
#25456=CARTESIAN_POINT('Ctrl Pts',(-1.50765390340601,-1.53610379571154,
5.29110235311216));
#25457=CARTESIAN_POINT('Ctrl Pts',(0.472410578590484,-2.0998723307505,5.40221429341067));
#25458=CARTESIAN_POINT('Ctrl Pts',(2.02025744064608,-0.742425510448462,
5.51332623370916));
#25459=CARTESIAN_POINT('Ctrl Pts',(1.71972992571626,1.29428083705086,5.62443817400769));
#25460=CARTESIAN_POINT('Ctrl Pts',(-0.154211925170411,2.14682455995381,
5.73555011430617));
#25461=CARTESIAN_POINT('Ctrl Pts',(-1.88706397163077,1.03519414292605,5.8466620546047));
#25462=CARTESIAN_POINT('Ctrl Pts',(-1.89340012825184,-1.02355328634819,
5.95777399490319));
#25463=CARTESIAN_POINT('Ctrl Pts',(-0.167433094557426,-2.14583667930556,
6.0688859352017));
#25464=CARTESIAN_POINT('Ctrl Pts',(1.71173403408707,-1.3048411079894,6.17999787550022));
#25465=CARTESIAN_POINT('Ctrl Pts',(2.02477823689865,0.729960380928156,6.29110981579872));
#25466=CARTESIAN_POINT('Ctrl Pts',(0.485356699136765,2.09694325990492,6.40222175609723));
#25467=CARTESIAN_POINT('Ctrl Pts',(-1.49821180042767,1.54532090104292,6.51333369639574));
#25468=CARTESIAN_POINT('Ctrl Pts',(-2.11087556882117,-0.420013146710507,
6.62444563669424));
#25469=CARTESIAN_POINT('Ctrl Pts',(-0.792563517738235,-2.00132267958093,
6.73555757699275));
#25470=CARTESIAN_POINT('Ctrl Pts',(1.2514647512946,-1.75109825238519,6.84666951729126));
#25471=CARTESIAN_POINT('Ctrl Pts',(2.1493875297017,0.100317623388547,6.95778145758976));
#25472=CARTESIAN_POINT('Ctrl Pts',(1.08294217967889,1.86172354306503,7.06889339788828));
#25473=CARTESIAN_POINT('Ctrl Pts',(-0.978616283938414,1.91630519923899,
7.18000533818678));
#25474=CARTESIAN_POINT('Ctrl Pts',(-1.74948643933749,0.788988358607273,
7.25407996505245));
#25475=CARTESIAN_POINT('Ctrl Pts',(-1.8115673562881,0.186739769222141,7.29111727848529));
#25476=CARTESIAN_POINT('Ctrl Pts',(0.980771099081382,-1.37424797458506,
-0.0766913607573567));
#25477=CARTESIAN_POINT('Ctrl Pts',(1.43763454458697,-1.04819440065571,-0.0396540473245209));
#25478=CARTESIAN_POINT('Ctrl Pts',(1.99276307249889,0.0896832201672716,
0.034420579541151));
#25479=CARTESIAN_POINT('Ctrl Pts',(1.00391299597902,1.72595584177028,0.145532519839658));
#25480=CARTESIAN_POINT('Ctrl Pts',(-0.904280198033752,1.77804327802189,
0.256644460138166));
#25481=CARTESIAN_POINT('Ctrl Pts',(-1.98468606023822,0.205907971189911,
0.367756400436673));
#25482=CARTESIAN_POINT('Ctrl Pts',(-1.24949583869046,-1.55593866201325,
0.478868340735181));
#25483=CARTESIAN_POINT('Ctrl Pts',(0.629005328535562,-1.89353353523676,
0.589980281033688));
#25484=CARTESIAN_POINT('Ctrl Pts',(1.93195278350834,-0.499060036321655,
0.701092221332196));
#25485=CARTESIAN_POINT('Ctrl Pts',(1.46735172982485,1.35220414221434,0.812204161630702));
#25486=CARTESIAN_POINT('Ctrl Pts',(-0.339776417673698,1.96620964359423,
0.923316101929211));
#25487=CARTESIAN_POINT('Ctrl Pts',(-1.8360270502188,0.781343207854476,1.03442804222772));
#25488=CARTESIAN_POINT('Ctrl Pts',(-1.65246473002849,-1.11841731974236,
1.14553998252623));
#25489=CARTESIAN_POINT('Ctrl Pts',(0.0429731402134002,-1.99490102020845,
1.25665192282473));
#25490=CARTESIAN_POINT('Ctrl Pts',(1.69909268320277,-1.04621752681478,1.36776386312324));
#25491=CARTESIAN_POINT('Ctrl Pts',(1.80067909324543,0.859675271613291,1.47887580342175));
#25492=CARTESIAN_POINT('Ctrl Pts',(0.254787859515066,1.97903189621542,1.58998774372026));
#25493=CARTESIAN_POINT('Ctrl Pts',(-1.52421368241876,1.2877338042565,1.70109968401876));
#25494=CARTESIAN_POINT('Ctrl Pts',(-1.90868177976625,-0.581738246844747,
1.81221162431727));
#25495=CARTESIAN_POINT('Ctrl Pts',(-0.54685873442858,-1.91896605181315,
1.92332356461578));
#25496=CARTESIAN_POINT('Ctrl Pts',(1.3152962632822,-1.50049364073057,2.03443550491428));
#25497=CARTESIAN_POINT('Ctrl Pts',(1.97406044940342,0.290810460411716,2.14554744521279));
#25498=CARTESIAN_POINT('Ctrl Pts',(0.826717287733271,1.81604621811011,2.2566593855113));
#25499=CARTESIAN_POINT('Ctrl Pts',(-1.0770060313669,1.6797450355543,2.36777132580981));
#25500=CARTESIAN_POINT('Ctrl Pts',(-1.99535501965367,0.00661155240574004,
2.47888326610832));
#25501=CARTESIAN_POINT('Ctrl Pts',(-1.08811383905831,-1.67257096577485,
2.58999520640682));
#25502=CARTESIAN_POINT('Ctrl Pts',(0.814664429048569,-1.82148489852237,
2.70110714670533));
#25503=CARTESIAN_POINT('Ctrl Pts',(1.97208993715443,-0.303885908906504,
2.81221908700384));
#25504=CARTESIAN_POINT('Ctrl Pts',(1.32521096607054,1.49174436843859,2.92333102730234));
#25505=CARTESIAN_POINT('Ctrl Pts',(-0.534129990910586,1.92254792369583,
3.03444296760085));
#25506=CARTESIAN_POINT('Ctrl Pts',(-1.90478474918523,0.594373977463801,
3.14555490789936));
#25507=CARTESIAN_POINT('Ctrl Pts',(-1.53271388940651,-1.27760459415048,
3.25666684819786));
#25508=CARTESIAN_POINT('Ctrl Pts',(0.241667526092368,-1.98067720053176,
3.36777878849638));
#25509=CARTESIAN_POINT('Ctrl Pts',(1.79494249429468,-0.871588669041957,
3.47889072879488));
#25510=CARTESIAN_POINT('Ctrl Pts',(1.70598871773261,1.03493374705916,3.59000266909339));
#25511=CARTESIAN_POINT('Ctrl Pts',(0.0561917835699789,1.99457460359148,
3.70111460939189));
#25512=CARTESIAN_POINT('Ctrl Pts',(-1.64501613589106,1.12933931060827,3.81222654969041));
#25513=CARTESIAN_POINT('Ctrl Pts',(-1.8411659309162,-0.769151077947235,
3.92333848998891));
#25514=CARTESIAN_POINT('Ctrl Pts',(-0.352796235600697,-1.96392978029257,
4.03445043028742));
#25515=CARTESIAN_POINT('Ctrl Pts',(1.45835378325819,-1.36186989417907,4.14556237058593));
#25516=CARTESIAN_POINT('Ctrl Pts',(1.93522679306129,0.486191963647073,4.25667431088443));
#25517=CARTESIAN_POINT('Ctrl Pts',(0.641522150567798,1.88942708133782,4.36778625118295));
#25518=CARTESIAN_POINT('Ctrl Pts',(-1.23912392249396,1.56398761841675,4.47889819148144));
#25519=CARTESIAN_POINT('Ctrl Pts',(-1.9860707661797,-0.192375360242598,
4.59001013177996));
#25520=CARTESIAN_POINT('Ctrl Pts',(-0.915921789707908,-1.77273027769074,
4.70112207207846));
#25521=CARTESIAN_POINT('Ctrl Pts',(0.992222326509824,-1.73117885322625,
4.81223401237697));
#25522=CARTESIAN_POINT('Ctrl Pts',(1.99256241999608,-0.105737308880805,
4.92334595267548));
#25523=CARTESIAN_POINT('Ctrl Pts',(1.1698673414902,1.61644540379926,5.03445789297399));
#25524=CARTESIAN_POINT('Ctrl Pts',(-0.723162719652709,1.85970994047142,
5.1455698332725));
#25525=CARTESIAN_POINT('Ctrl Pts',(-1.95455679656824,0.401488673645819,
5.25668177357099));
#25526=CARTESIAN_POINT('Ctrl Pts',(-1.39768774974859,-1.42406254695323,
5.36779371386952));
#25527=CARTESIAN_POINT('Ctrl Pts',(0.437953615916691,-1.94671059856343,
5.47890565416801));
#25528=CARTESIAN_POINT('Ctrl Pts',(1.87290270648346,-0.688274038697066,
5.59001759446653));
#25529=CARTESIAN_POINT('Ctrl Pts',(1.59429524549334,1.19987781452597,5.70112953476503));
#25530=CARTESIAN_POINT('Ctrl Pts',(-0.142963924405265,1.99023819825497,
5.81224147506354));
#25531=CARTESIAN_POINT('Ctrl Pts',(-1.74942418162531,0.959688539200224,
5.92335341536204));
#25532=CARTESIAN_POINT('Ctrl Pts',(-1.75529818790071,-0.948896750316397,
6.03446535566056));
#25533=CARTESIAN_POINT('Ctrl Pts',(-0.155220760306272,-1.98932237223074,
6.14557729595905));
#25534=CARTESIAN_POINT('Ctrl Pts',(1.58688256294519,-1.20966783416606,6.25668923625758));
#25535=CARTESIAN_POINT('Ctrl Pts',(1.8770937622205,0.676718098179033,6.36780117655607));
#25536=CARTESIAN_POINT('Ctrl Pts',(0.449955464652266,1.94399517002259,6.47891311685458));
#25537=CARTESIAN_POINT('Ctrl Pts',(-1.38893434047152,1.43260736959501,6.59002505715309));
#25538=CARTESIAN_POINT('Ctrl Pts',(-1.95691127593653,-0.389377978967469,
6.7011369974516));
#25539=CARTESIAN_POINT('Ctrl Pts',(-0.734755050305503,-1.8553490202393,
6.8122489377501));
#25540=CARTESIAN_POINT('Ctrl Pts',(1.16018467380016,-1.62337561056666,6.92336087804862));
#25541=CARTESIAN_POINT('Ctrl Pts',(1.99261422859689,0.0930005971379224,
7.03447281834711));
#25542=CARTESIAN_POINT('Ctrl Pts',(1.00395390135875,1.72593204825193,7.14558475864564));
#25543=CARTESIAN_POINT('Ctrl Pts',(-0.907237389612538,1.77653259524947,
7.25669669894413));
#25544=CARTESIAN_POINT('Ctrl Pts',(-1.62188136089401,0.731440658249439,
7.33077132580981));
#25545=CARTESIAN_POINT('Ctrl Pts',(-1.67943418314253,0.173119233295526,
7.36780863924264));
#25546=CARTESIAN_POINT('Ctrl Pts',(0.903606778650207,-1.26612599672284,
-1.38777878078145E-15));
#25547=CARTESIAN_POINT('Ctrl Pts',(1.32452548910467,-0.965725403881512,
0.0370373134328344));
#25548=CARTESIAN_POINT('Ctrl Pts',(1.83597806077316,0.082627195836251,0.111111940298506));
#25549=CARTESIAN_POINT('Ctrl Pts',(0.924927935979477,1.59016247494986,0.222223880597014));
#25550=CARTESIAN_POINT('Ctrl Pts',(-0.833133967250649,1.63815181774712,
0.333335820895521));
#25551=CARTESIAN_POINT('Ctrl Pts',(-1.82853652519283,0.189707709290757,
0.444447761194028));
#25552=CARTESIAN_POINT('Ctrl Pts',(-1.15118900913109,-1.43352177024381,
0.555559701492536));
#25553=CARTESIAN_POINT('Ctrl Pts',(0.579516952736672,-1.74455562530747,
0.666671641791043));
#25554=CARTESIAN_POINT('Ctrl Pts',(1.77995215483547,-0.45979539180552,0.777783582089551));
#25555=CARTESIAN_POINT('Ctrl Pts',(1.35190460952174,1.24581651128198,0.888895522388059));
#25556=CARTESIAN_POINT('Ctrl Pts',(-0.313043761712607,1.81151378121076,
1.00000746268657));
#25557=CARTESIAN_POINT('Ctrl Pts',(-1.6915735893082,0.719869314798195,1.11111940298507));
#25558=CARTESIAN_POINT('Ctrl Pts',(-1.52245343784362,-1.03042338056816,
1.22223134328358));
#25559=CARTESIAN_POINT('Ctrl Pts',(0.0395921340189295,-1.83794780075079,
1.33334328358209));
#25560=CARTESIAN_POINT('Ctrl Pts',(1.56541283438613,-0.96390406493211,1.44445522388059));
#25561=CARTESIAN_POINT('Ctrl Pts',(1.65900671048959,0.792038431388639,1.55556716417911));
#25562=CARTESIAN_POINT('Ctrl Pts',(0.234741865039883,1.82332721494359,1.66667910447761));
#25563=CARTESIAN_POINT('Ctrl Pts',(-1.40429282310112,1.18641851876859,1.77779104477612));
#25564=CARTESIAN_POINT('Ctrl Pts',(-1.7585120484263,-0.535968712517482,
1.88890298507462));
#25565=CARTESIAN_POINT('Ctrl Pts',(-0.503833422351614,-1.76798718278107,
2.00001492537314));
#25566=CARTESIAN_POINT('Ctrl Pts',(1.211812440791,-1.38243900779253,2.11112686567164));
#25567=CARTESIAN_POINT('Ctrl Pts',(1.81874690762903,0.2679303086893,2.22223880597015));
#25568=CARTESIAN_POINT('Ctrl Pts',(0.761673489280804,1.67316479305249,2.33335074626865));
#25569=CARTESIAN_POINT('Ctrl Pts',(-0.99227021626331,1.54758740541246,2.44446268656716));
#25570=CARTESIAN_POINT('Ctrl Pts',(-1.83836608079246,0.00609137399829168,
2.55557462686567));
#25571=CARTESIAN_POINT('Ctrl Pts',(-1.00250409278689,-1.54097777133038,
2.66668656716418));
#25572=CARTESIAN_POINT('Ctrl Pts',(0.750568915726592,-1.67817557333754,
2.77779850746269));
#25573=CARTESIAN_POINT('Ctrl Pts',(1.81693142975936,-0.279977017554228,
2.8889104477612));
#25574=CARTESIAN_POINT('Ctrl Pts',(1.22094708256035,1.37437810371544,3.0000223880597));
#25575=CARTESIAN_POINT('Ctrl Pts',(-0.492106140687917,1.77128724302598,
3.11113432835821));
#25576=CARTESIAN_POINT('Ctrl Pts',(-1.75492162528586,0.547610299276366,
3.22224626865671));
#25577=CARTESIAN_POINT('Ctrl Pts',(-1.41212425763385,-1.17708624651594,
3.33335820895523));
#25578=CARTESIAN_POINT('Ctrl Pts',(0.222653802667342,-1.82484307132901,
3.44447014925373));
#25579=CARTESIAN_POINT('Ctrl Pts',(1.65372145106143,-0.803014516107455,
3.55558208955224));
#25580=CARTESIAN_POINT('Ctrl Pts',(1.57176630825256,0.953508061332994,3.66669402985075));
#25581=CARTESIAN_POINT('Ctrl Pts',(0.0517707715753711,1.83764706567811,
3.77780597014925));
#25582=CARTESIAN_POINT('Ctrl Pts',(-1.5155908782104,1.04048605981312,3.88891791044777));
#25583=CARTESIAN_POINT('Ctrl Pts',(-1.69630815727945,-0.708636427490783,
4.00002985074626));
#25584=CARTESIAN_POINT('Ctrl Pts',(-0.325039216866852,-1.80941329116195,
4.11114179104478));
#25585=CARTESIAN_POINT('Ctrl Pts',(1.34361459616473,-1.25472178898058,4.22225373134328));
#25586=CARTESIAN_POINT('Ctrl Pts',(1.78296857449566,0.447939743012656,4.3333656716418));
#25587=CARTESIAN_POINT('Ctrl Pts',(0.591048986302979,1.74077225568864,4.44447761194029));
#25588=CARTESIAN_POINT('Ctrl Pts',(-1.14163312622272,1.44093745732314,4.55558955223881));
#25589=CARTESIAN_POINT('Ctrl Pts',(-1.82981228635293,-0.177239806233389,
4.66670149253731));
#25590=CARTESIAN_POINT('Ctrl Pts',(-0.843859631129698,-1.63325682938675,
4.77781343283583));
#25591=CARTESIAN_POINT('Ctrl Pts',(0.914157055608714,-1.59497455450745,
4.88892537313433));
#25592=CARTESIAN_POINT('Ctrl Pts',(1.83579319504673,-0.0974181938582904,
5.00003731343284));
#25593=CARTESIAN_POINT('Ctrl Pts',(1.07782545884778,1.48926801121999,5.11114925373134));
#25594=CARTESIAN_POINT('Ctrl Pts',(-0.666266304296033,1.713393176152,5.22226119402985));
#25595=CARTESIAN_POINT('Ctrl Pts',(-1.80077774751939,0.369900670398456,
5.33337313432836));
#25596=CARTESIAN_POINT('Ctrl Pts',(-1.28772159609117,-1.31202129819493,
5.44448507462686));
#25597=CARTESIAN_POINT('Ctrl Pts',(0.403496653242899,-1.79354886637635,
5.55559701492538));
#25598=CARTESIAN_POINT('Ctrl Pts',(1.72554797232085,-0.634122566945669,
5.66670895522387));
#25599=CARTESIAN_POINT('Ctrl Pts',(1.46886056527041,1.10547479200108,5.77782089552239));
#25600=CARTESIAN_POINT('Ctrl Pts',(-0.131715923640121,1.83365183655613,
5.88893283582089));
#25601=CARTESIAN_POINT('Ctrl Pts',(-1.61178439161985,0.884182935474394,
6.0000447761194));
#25602=CARTESIAN_POINT('Ctrl Pts',(-1.61719624754958,-0.874240214284601,
6.11115671641792));
#25603=CARTESIAN_POINT('Ctrl Pts',(-0.143008426055117,-1.83280806515592,
6.2222686567164));
#25604=CARTESIAN_POINT('Ctrl Pts',(1.4620310918033,-1.11449456034272,6.33338059701493));
#25605=CARTESIAN_POINT('Ctrl Pts',(1.72940928754233,0.623475815429911,6.44449253731343));
#25606=CARTESIAN_POINT('Ctrl Pts',(0.414554230167772,1.79104708014026,6.55560447761194));
#25607=CARTESIAN_POINT('Ctrl Pts',(-1.27965688051538,1.3198938381471,6.66671641791045));
#25608=CARTESIAN_POINT('Ctrl Pts',(-1.80294698305189,-0.358742811224428,
6.77782835820896));
#25609=CARTESIAN_POINT('Ctrl Pts',(-0.676946582872774,-1.70937536089767,
6.88894029850746));
#25610=CARTESIAN_POINT('Ctrl Pts',(1.06890459630572,-1.49565296874813,7.00005223880597));
#25611=CARTESIAN_POINT('Ctrl Pts',(1.83584092749207,0.0856835708872964,
7.11116417910447));
#25612=CARTESIAN_POINT('Ctrl Pts',(0.924965623038614,1.59014055343882,7.22227611940298));
#25613=CARTESIAN_POINT('Ctrl Pts',(-0.835858495286665,1.63675999125994,
7.33338805970149));
#25614=CARTESIAN_POINT('Ctrl Pts',(-1.49427628245053,0.673892957891604,
7.40746268656716));
#25615=CARTESIAN_POINT('Ctrl Pts',(-1.54730100999696,0.159498697368912,
7.4445));
#25616=CARTESIAN_POINT('',(0.903606778650208,-1.26612599672284,0.));
#25617=CARTESIAN_POINT('Ctrl Pts',(0.903606778650207,-1.26612599672284,
-1.38777878078145E-15));
#25618=CARTESIAN_POINT('Ctrl Pts',(1.32452548910467,-0.965725403881512,
0.0370373134328344));
#25619=CARTESIAN_POINT('Ctrl Pts',(1.83597806077316,0.082627195836251,0.111111940298506));
#25620=CARTESIAN_POINT('Ctrl Pts',(0.924927935979477,1.59016247494986,0.222223880597014));
#25621=CARTESIAN_POINT('Ctrl Pts',(-0.833133967250649,1.63815181774712,
0.333335820895521));
#25622=CARTESIAN_POINT('Ctrl Pts',(-1.5310648992002,0.622568787117098,0.411242452161949));
#25623=CARTESIAN_POINT('Ctrl Pts',(-1.55772948793458,0.0543297678623362,
0.452111769995541));
#25624=CARTESIAN_POINT('Ctrl Pts',(-1.55735958542387,0.00101297198046621,
0.455943774396298));
#25625=CARTESIAN_POINT('Ctrl Pts',(0.863568564283469,1.75641400930303,0.));
#25626=CARTESIAN_POINT('Ctrl Pts',(0.902603531943078,1.7324423702308,2.28859211685802E-17));
#25627=CARTESIAN_POINT('Ctrl Pts',(0.940676776691071,1.70703651305647,-1.38032481715684E-16));
#25628=CARTESIAN_POINT('Ctrl Pts',(0.977697814042708,1.68019172043607,-1.28369537222284E-16));
#25629=CARTESIAN_POINT('Ctrl Pts',(1.03585714935899,1.63801906923031,-1.20927094907836E-16));
#25630=CARTESIAN_POINT('Ctrl Pts',(1.09142188330105,1.59229630788867,-2.7046412047637E-16));
#25631=CARTESIAN_POINT('Ctrl Pts',(1.14423064795477,1.54336420856895,-1.97758476261356E-16));
#25632=CARTESIAN_POINT('Ctrl Pts',(1.16946834979149,1.51997919396061,-1.63011907532148E-16));
#25633=CARTESIAN_POINT('Ctrl Pts',(1.19407597424497,1.49586072902399,-7.62289135782024E-17));
#25634=CARTESIAN_POINT('Ctrl Pts',(1.21803226410959,1.47104407323701,-6.59194920871187E-17));
#25635=CARTESIAN_POINT('Ctrl Pts',(1.23017793652576,1.45846220127952,-6.0692687062697E-17));
#25636=CARTESIAN_POINT('Ctrl Pts',(1.24215614940632,1.44570084965787,-2.95883426371776E-16));
#25637=CARTESIAN_POINT('Ctrl Pts',(1.25396388375076,1.43276453675822,-3.36536354339501E-16));
#25638=CARTESIAN_POINT('Ctrl Pts',(1.2638543668245,1.42192872524363,-3.70588365016071E-16));
#25639=CARTESIAN_POINT('Ctrl Pts',(1.2736185550329,1.41097745381189,1.09305947039191E-16));
#25640=CARTESIAN_POINT('Ctrl Pts',(1.28325381741352,1.39991535359824,9.71445146547012E-17));
#25641=CARTESIAN_POINT('Ctrl Pts',(1.33014189367208,1.34608385655041,3.79633375853411E-17));
#25642=CARTESIAN_POINT('Ctrl Pts',(1.37399192615748,1.28961736627304,-2.11573378166283E-16));
#25643=CARTESIAN_POINT('Ctrl Pts',(1.4146405205773,1.23085017638072,-2.98372437868011E-16));
#25644=CARTESIAN_POINT('Ctrl Pts',(1.44368223570237,1.18886348503472,-3.60386723994296E-16));
#25645=CARTESIAN_POINT('Ctrl Pts',(1.47108885988106,1.14570172941536,-3.55315850605615E-16));
#25646=CARTESIAN_POINT('Ctrl Pts',(1.49678522627473,1.10148200990233,-3.88578058618805E-16));
#25647=CARTESIAN_POINT('Ctrl Pts',(1.51163132719121,1.07593402353214,-4.0779533196023E-16));
#25648=CARTESIAN_POINT('Ctrl Pts',(1.52590630204136,1.05003284136309,-4.46468072791598E-16));
#25649=CARTESIAN_POINT('Ctrl Pts',(1.53959352057452,1.02380089191946,-4.5102810375397E-16));
#25650=CARTESIAN_POINT('Ctrl Pts',(1.54536419749809,1.0127412230066,-4.5295066131244E-16));
#25651=CARTESIAN_POINT('Ctrl Pts',(1.55102598614157,1.00163115224642,-3.28801907372083E-16));
#25652=CARTESIAN_POINT('Ctrl Pts',(1.55657733146951,0.990474109820403,-3.19189119579733E-16));
#25653=CARTESIAN_POINT('Ctrl Pts',(1.58759135376405,0.928142415050821,-2.65484801564386E-16));
#25654=CARTESIAN_POINT('Ctrl Pts',(1.61517084797965,0.864329379202861,-6.67259587666608E-16));
#25655=CARTESIAN_POINT('Ctrl Pts',(1.6391617363075,0.799343273084874,-5.82867087928207E-16));
#25656=CARTESIAN_POINT('Ctrl Pts',(1.66256147081466,0.735958474279834,-5.00554083870677E-16));
#25657=CARTESIAN_POINT('Ctrl Pts',(1.68254736306605,0.671456731546573,9.30631015772363E-17));
#25658=CARTESIAN_POINT('Ctrl Pts',(1.69892809919455,0.606119085630755,1.11022302462516E-16));
#25659=CARTESIAN_POINT('Ctrl Pts',(1.70969727271493,0.563164212250211,1.2282920473501E-16));
#25660=CARTESIAN_POINT('Ctrl Pts',(1.71890726464806,0.519847981128071,-1.31890518419189E-16));
#25661=CARTESIAN_POINT('Ctrl Pts',(1.72649157325935,0.476251973430995,-1.38777878078145E-16));
#25662=CARTESIAN_POINT('Ctrl Pts',(1.73286785345701,0.439599936333954,-1.44568219328534E-16));
#25663=CARTESIAN_POINT('Ctrl Pts',(1.73809492661148,0.402750145627894,-3.72078883249312E-16));
#25664=CARTESIAN_POINT('Ctrl Pts',(1.74212769993621,0.365752815321986,-4.16333634234434E-16));
#25665=CARTESIAN_POINT('Ctrl Pts',(1.74338298809393,0.354236593888137,-4.30108885249319E-16));
#25666=CARTESIAN_POINT('Ctrl Pts',(1.7445224615788,0.34270569873049,-4.2222380310258E-18));
#25667=CARTESIAN_POINT('Ctrl Pts',(1.74554359854572,0.331176868161872,-1.38777878078145E-17));
#25668=CARTESIAN_POINT('Ctrl Pts',(1.75129265664821,0.266268908759598,-6.82390718242887E-17));
#25669=CARTESIAN_POINT('Ctrl Pts',(1.75330855751176,0.201308359017101,-1.61972025925174E-16));
#25670=CARTESIAN_POINT('Ctrl Pts',(1.75142416657778,0.13655560768634,-1.38777878078145E-16));
#25671=CARTESIAN_POINT('Ctrl Pts',(1.75088156113035,0.117910222074166,-1.32099183788468E-16));
#25672=CARTESIAN_POINT('Ctrl Pts',(1.75001524326664,0.0992821075343112,
-1.58618989379829E-17));
#25673=CARTESIAN_POINT('Ctrl Pts',(1.74882042289714,0.0806776277944099,
0.));
#25674=CARTESIAN_POINT('Ctrl Pts',(1.74441970791246,0.0121543460832101,
6.07280452025807E-17));
#25675=CARTESIAN_POINT('Ctrl Pts',(1.735566761163,-0.0560504444942819,-6.11382253507945E-17));
#25676=CARTESIAN_POINT('Ctrl Pts',(1.72245455146386,-0.123599567095003,
-1.38777878078145E-16));
#25677=CARTESIAN_POINT('Ctrl Pts',(1.7106535204694,-0.184393995170097,-2.08653815792513E-16));
#25678=CARTESIAN_POINT('Ctrl Pts',(1.69540126258663,-0.244657625690558,
-3.30909447568271E-16));
#25679=CARTESIAN_POINT('Ctrl Pts',(1.67680583516799,-0.304119468797943,
-3.05311331771918E-16));
#25680=CARTESIAN_POINT('Ctrl Pts',(1.673496966793,-0.314700102829495,-3.00756405772578E-16));
#25681=CARTESIAN_POINT('Ctrl Pts',(1.67008375904048,-0.325250056291554,
1.12130257435328E-16));
#25682=CARTESIAN_POINT('Ctrl Pts',(1.66656954022458,-0.335760782955591,
1.11022302462516E-16));
#25683=CARTESIAN_POINT('Ctrl Pts',(1.64601748634937,-0.397230211008769,
1.04542697325368E-16));
#25684=CARTESIAN_POINT('Ctrl Pts',(1.62199078115275,-0.457436083404927,
4.89063387979405E-18));
#25685=CARTESIAN_POINT('Ctrl Pts',(1.59467603738004,-0.516104439016194,
-1.11022302462516E-16));
#25686=CARTESIAN_POINT('Ctrl Pts',(1.56746949320957,-0.574540396593861,
-2.26476082617573E-16));
#25687=CARTESIAN_POINT('Ctrl Pts',(1.53700015167997,-0.631451830043097,
-2.65447621135955E-16));
#25688=CARTESIAN_POINT('Ctrl Pts',(1.50341281573621,-0.68653552753498,-3.60822483003176E-16));
#25689=CARTESIAN_POINT('Ctrl Pts',(1.4705131167318,-0.740491490894733,-4.54244725638714E-16));
#25690=CARTESIAN_POINT('Ctrl Pts',(1.43462103920338,-0.792694411910378,
-4.2831431104574E-16));
#25691=CARTESIAN_POINT('Ctrl Pts',(1.39584581076301,-0.842817530414533,
-5.27355936696949E-16));
#25692=CARTESIAN_POINT('Ctrl Pts',(1.38890062306969,-0.851795284506205,
-5.45095682077361E-16));
#25693=CARTESIAN_POINT('Ctrl Pts',(1.38186288427344,-0.860706190744767,
2.35960662867998E-16));
#25694=CARTESIAN_POINT('Ctrl Pts',(1.37473315631241,-0.86954820289757,2.4980018054066E-16));
#25695=CARTESIAN_POINT('Ctrl Pts',(1.36794195322354,-0.877970389630667,
2.62982587454478E-16));
#25696=CARTESIAN_POINT('Ctrl Pts',(1.36107048536455,-0.886326025058287,
-6.35152333120316E-18));
#25697=CARTESIAN_POINT('Ctrl Pts',(1.35412452302825,-0.894607674989563,
0.));
#25698=CARTESIAN_POINT('Ctrl Pts',(1.31424959800426,-0.942150427756674,
3.64624085702422E-17));
#25699=CARTESIAN_POINT('Ctrl Pts',(1.2718724912058,-0.987319961554271,-3.18360401148313E-16));
#25700=CARTESIAN_POINT('Ctrl Pts',(1.22713193424969,-1.02984905091596,-2.22044604925031E-16));
#25701=CARTESIAN_POINT('Ctrl Pts',(1.18319618732353,-1.0716131109617,-1.27461373607439E-16));
#25702=CARTESIAN_POINT('Ctrl Pts',(1.13698054744349,-1.11083140282356,-2.10671899724563E-16));
#25703=CARTESIAN_POINT('Ctrl Pts',(1.08859303083371,-1.14720695088303,-2.77555756156289E-16));
#25704=CARTESIAN_POINT('Ctrl Pts',(1.04174975410163,-1.18242160919609,-3.42305080264122E-16));
#25705=CARTESIAN_POINT('Ctrl Pts',(0.992870408249348,-1.21497237243561,
-3.26158703430296E-16));
#25706=CARTESIAN_POINT('Ctrl Pts',(0.942040458977608,-1.24454244204819,
-3.60822483003176E-16));
#25707=CARTESIAN_POINT('Ctrl Pts',(0.92935042596986,-1.25192480549339,-3.69476524828035E-16));
#25708=CARTESIAN_POINT('Ctrl Pts',(0.916538776387811,-1.25912113789668,
-6.13893683198417E-17));
#25709=CARTESIAN_POINT('Ctrl Pts',(0.903606778650223,-1.26612599672282,
-5.55111512312578E-17));
#25710=CARTESIAN_POINT('Ctrl Pts',(0.0849160311154397,1.9485495525967,7.04599999999999));
#25711=CARTESIAN_POINT('Ctrl Pts',(0.400605874250757,1.93520776532856,7.0280673457103));
#25712=CARTESIAN_POINT('Ctrl Pts',(0.713151734000586,1.84952766933244,7.01013469142061));
#25713=CARTESIAN_POINT('Ctrl Pts',(0.983981247423036,1.69229543406338,6.99220203713092));
#25714=CARTESIAN_POINT('Ctrl Pts',(1.54334058226818,1.36755490846516,6.95516472369808));
#25715=CARTESIAN_POINT('Ctrl Pts',(1.92475070653735,0.737594779052165,6.91812741026524));
#25716=CARTESIAN_POINT('Ctrl Pts',(1.95488643500235,0.0915387903718514,
6.88109009683241));
#25717=CARTESIAN_POINT('Ctrl Pts',(1.98502216346735,-0.554517198308454,
6.84405278339957));
#25718=CARTESIAN_POINT('Ctrl Pts',(1.6638834961282,-1.21666904625608,6.80701546996674));
#25719=CARTESIAN_POINT('Ctrl Pts',(1.13779469346529,-1.59249087768303,6.7699781565339));
#25720=CARTESIAN_POINT('Ctrl Pts',(0.611705890802371,-1.96831270910999,
6.73294084310107));
#25721=CARTESIAN_POINT('Ctrl Pts',(-0.119333047184302,-2.05780452401628,
6.69590352966823));
#25722=CARTESIAN_POINT('Ctrl Pts',(-0.720597162266781,-1.81977576072458,
6.65886621623539));
#25723=CARTESIAN_POINT('Ctrl Pts',(-1.32186127734926,-1.58174699743288,
6.62182890280256));
#25724=CARTESIAN_POINT('Ctrl Pts',(-1.79335056952755,-1.0161976559432,6.58479158936972));
#25725=CARTESIAN_POINT('Ctrl Pts',(-1.91953678206301,-0.381975860707627,
6.54775427593688));
#25726=CARTESIAN_POINT('Ctrl Pts',(-1.94439039128642,-0.257059672615188,
6.540459414666));
#25727=CARTESIAN_POINT('Ctrl Pts',(-1.9558486040335,-0.129479463263859,
6.53316455339512));
#25728=CARTESIAN_POINT('Ctrl Pts',(-1.95467666345581,-0.00169153748172557,
6.52586969212423));
#25729=CARTESIAN_POINT('Origin',(0.,0.,-1.2940562256037));
#25730=CARTESIAN_POINT('',(-0.903606778650191,-1.26612599672285,1.38777878078145E-16));
#25731=CARTESIAN_POINT('Ctrl Pts',(-0.905552056217056,-1.26793026328003,
8.26433105977076E-16));
#25732=CARTESIAN_POINT('Ctrl Pts',(-0.513280080436939,-1.54506079646518,
0.0345343505799217));
#25733=CARTESIAN_POINT('Ctrl Pts',(0.58913651448779,-1.72157402054048,0.106143938272268));
#25734=CARTESIAN_POINT('Ctrl Pts',(1.77597071143275,-0.477272995959146,
0.214828763077039));
#25735=CARTESIAN_POINT('Ctrl Pts',(1.3630442868689,1.23477489449879,0.326054474414316));
#25736=CARTESIAN_POINT('Ctrl Pts',(-0.299513989741265,1.81437004394786,
0.437280185751592));
#25737=CARTESIAN_POINT('Ctrl Pts',(-1.41424275662139,0.944368549815884,
0.526614102814722));
#25738=CARTESIAN_POINT('Ctrl Pts',(-1.55418552513067,0.213449522874851,
0.578872782765425));
#25739=CARTESIAN_POINT('Ctrl Pts',(-1.55327638232574,0.000749985450955847,
0.594056225603703));
#25740=CARTESIAN_POINT('Origin',(0.,0.,0.));
#25741=CARTESIAN_POINT('Ctrl Pts',(-0.685825729128727,1.39614588036675,
-0.230074082272066));
#25742=CARTESIAN_POINT('Ctrl Pts',(-1.15044430012221,1.1679123019855,-0.19299884515964));
#25743=CARTESIAN_POINT('Ctrl Pts',(-1.8258407957124,0.215070471435756,-0.118848370934789));
#25744=CARTESIAN_POINT('Ctrl Pts',(-1.16856980438922,-1.42158824274557,
-0.0076226595975132));
#25745=CARTESIAN_POINT('Ctrl Pts',(0.561390129169046,-1.75066389321976,
0.103603051739764));
#25746=CARTESIAN_POINT('Ctrl Pts',(1.77597071143275,-0.477272995959146,
0.214828763077039));
#25747=CARTESIAN_POINT('Ctrl Pts',(1.3630442868689,1.23477489449879,0.326054474414316));
#25748=CARTESIAN_POINT('Ctrl Pts',(-0.299513989741265,1.81437004394786,
0.437280185751592));
#25749=CARTESIAN_POINT('Ctrl Pts',(-1.68741350339127,0.731169639996686,
0.548505897088869));
#25750=CARTESIAN_POINT('Ctrl Pts',(-1.52862817745114,-1.02241621535808,
0.659731608426144));
#25751=CARTESIAN_POINT('Ctrl Pts',(0.0313843551128396,-1.83872969125081,
0.770957319763422));
#25752=CARTESIAN_POINT('Ctrl Pts',(1.56261245507102,-0.969643437172017,
0.882183031100698));
#25753=CARTESIAN_POINT('Ctrl Pts',(1.66150197094076,0.788277540412492,0.993408742437974));
#25754=CARTESIAN_POINT('Ctrl Pts',(0.237394066880885,1.82362194812979,1.10463445377525));
#25755=CARTESIAN_POINT('Ctrl Pts',(-1.40431546877471,1.18737513564603,1.21586016511253));
#25756=CARTESIAN_POINT('Ctrl Pts',(-1.75877981175223,-0.537266275957094,
1.3270858764498));
#25757=CARTESIAN_POINT('Ctrl Pts',(-0.501082205369057,-1.76942810040879,
1.43831158778708));
#25758=CARTESIAN_POINT('Ctrl Pts',(1.21592516185098,-1.37966899434435,1.54953729912436));
#25759=CARTESIAN_POINT('Ctrl Pts',(1.8183716526183,0.274745208061178,1.66076301046163));
#25760=CARTESIAN_POINT('Ctrl Pts',(0.754032712405612,1.67731773070425,1.77198872179891));
#25761=CARTESIAN_POINT('Ctrl Pts',(-1.00147988107901,1.54240019271928,1.88321443313619));
#25762=CARTESIAN_POINT('Ctrl Pts',(-1.83899975790172,-0.00633731701985082,
1.99444014447346));
#25763=CARTESIAN_POINT('Ctrl Pts',(-0.990825815880477,-1.5492657736205,
2.10566585581074));
#25764=CARTESIAN_POINT('Ctrl Pts',(0.765574959497512,-1.6720811124538,2.21689156714802));
#25765=CARTESIAN_POINT('Ctrl Pts',(1.82022199392772,-0.262206313316451,
2.32811727848529));
#25766=CARTESIAN_POINT('Ctrl Pts',(1.20638759997596,1.38801628675575,2.43934298982257));
#25767=CARTESIAN_POINT('Ctrl Pts',(-0.513265374585843,1.76593287340023,
2.55056870115984));
#25768=CARTESIAN_POINT('Ctrl Pts',(-1.76244071170529,0.525131406868061,
2.66179441249712));
#25769=CARTESIAN_POINT('Ctrl Pts',(-1.39609903883734,-1.19702453193727,
2.77302012383439));
#25770=CARTESIAN_POINT('Ctrl Pts',(0.249957593646744,-1.82194441691009,
2.88424583517168));
#25771=CARTESIAN_POINT('Ctrl Pts',(1.6668940398915,-0.776804039943688,2.99547154650895));
#25772=CARTESIAN_POINT('Ctrl Pts',(1.55589501744036,0.980383063583733,3.10669725784622));
#25773=CARTESIAN_POINT('Ctrl Pts',(0.0187062518377651,1.83891553174339,
3.2179229691835));
#25774=CARTESIAN_POINT('Ctrl Pts',(-1.53562934193987,1.01183139943408,3.32914868052078));
#25775=CARTESIAN_POINT('Ctrl Pts',(-1.68235144492823,-0.742734052303713,
3.44037439185806));
#25776=CARTESIAN_POINT('Ctrl Pts',(-0.286969261786828,-1.81648256240041,
3.55160010319533));
#25777=CARTESIAN_POINT('Ctrl Pts',(1.37145934362907,-1.22517734450477,3.66282581453261));
#25778=CARTESIAN_POINT('Ctrl Pts',(1.77275862659963,0.489169815626649,3.77405152586988));
#25779=CARTESIAN_POINT('Ctrl Pts',(0.549083125265984,1.75512620009375,3.88527723720716));
#25780=CARTESIAN_POINT('Ctrl Pts',(-1.17790186202284,1.41227032121617,3.99650294854444));
#25781=CARTESIAN_POINT('Ctrl Pts',(-1.82517932708368,-0.225123700760077,
4.10772865988171));
#25782=CARTESIAN_POINT('Ctrl Pts',(-0.799431294618187,-1.65616118233816,
4.21895437121899));
#25783=CARTESIAN_POINT('Ctrl Pts',(0.959104426053338,-1.56910132141185,
4.33018008255627));
#25784=CARTESIAN_POINT('Ctrl Pts',(1.83849028118038,-0.0437463405035559,
4.44140579389354));
#25785=CARTESIAN_POINT('Ctrl Pts',(1.0326493363287,1.52170812080878,4.55263150523082));
#25786=CARTESIAN_POINT('Ctrl Pts',(-0.719755403894915,1.69230978744094,
4.6638572165681));
#25787=CARTESIAN_POINT('Ctrl Pts',(-1.81240626272056,0.311678989548955,
4.77508292790537));
#25788=CARTESIAN_POINT('Ctrl Pts',(-1.24373988019232,-1.35464806069341,
4.88630863924265));
#25789=CARTESIAN_POINT('Ctrl Pts',(0.464983542380115,-1.77925562259896,
4.99753435057992));
#25790=CARTESIAN_POINT('Ctrl Pts',(1.74748619395055,-0.572933012383953,
5.1087600619172));
#25791=CARTESIAN_POINT('Ctrl Pts',(1.42817970701863,1.15856074316792,5.21998577325448));
#25792=CARTESIAN_POINT('Ctrl Pts',(-0.20024807751692,1.82807576816643,5.33121148459175));
#25793=CARTESIAN_POINT('Ctrl Pts',(-1.64512115233065,0.821910272029074,
5.44243719592903));
#25794=CARTESIAN_POINT('Ctrl Pts',(-1.58201670345687,-0.937647879740503,
5.55366290726631));
#25795=CARTESIAN_POINT('Ctrl Pts',(-0.0687781849042931,-1.83772416168987,
5.66488861860358));
#25796=CARTESIAN_POINT('Ctrl Pts',(1.50750444735784,-1.05327561457109,5.77611432994086));
#25797=CARTESIAN_POINT('Ctrl Pts',(1.70195476716013,0.696642984640571,5.88734004127814));
#25798=CARTESIAN_POINT('Ctrl Pts',(0.336330007005007,1.80799440678846,5.99856575261541));
#25799=CARTESIAN_POINT('Ctrl Pts',(-1.33758382509627,1.26207070464844,6.10979146395269));
#25800=CARTESIAN_POINT('Ctrl Pts',(-1.78542595464098,-0.440709020390059,
6.22101717528996));
#25801=CARTESIAN_POINT('Ctrl Pts',(-0.59667036110871,-1.73952595846347,
6.33224288662724));
#25802=CARTESIAN_POINT('Ctrl Pts',(1.13899278941852,-1.44381691390763,6.44346859796452));
#25803=CARTESIAN_POINT('Ctrl Pts',(1.83065601360088,0.17532136832598,6.5546943093018));
#25804=CARTESIAN_POINT('Ctrl Pts',(0.844193344579619,1.63380261073593,6.66592002063907));
#25805=CARTESIAN_POINT('Ctrl Pts',(-0.915934603694247,1.5945880622222,6.77714573197635));
#25806=CARTESIAN_POINT('Ctrl Pts',(-1.83677508915277,0.093893769326276,
6.88837144331362));
#25807=CARTESIAN_POINT('Ctrl Pts',(-1.07340561084952,-1.49320523543669,
6.99959715465089));
#25808=CARTESIAN_POINT('Ctrl Pts',(0.672826183539381,-1.71093187207897,
7.11082286598819));
#25809=CARTESIAN_POINT('Ctrl Pts',(1.80435891657647,-0.361603954366771,
7.22204857732544));
#25810=CARTESIAN_POINT('Ctrl Pts',(1.27791236939833,1.32169962363241,7.33327428866273));
#25811=CARTESIAN_POINT('Ctrl Pts',(0.152038852759137,1.63230677878407,7.40742476288758));
#25812=CARTESIAN_POINT('Ctrl Pts',(-0.352169241380528,1.51510959188617,
7.44450000000001));
#25813=CARTESIAN_POINT('Ctrl Pts',(-0.744392439309327,1.51537102412035,
-0.153382721514711));
#25814=CARTESIAN_POINT('Ctrl Pts',(-1.24868753458029,1.26764723230613,-0.116307484402285));
#25815=CARTESIAN_POINT('Ctrl Pts',(-1.9817601264938,0.233436609412224,-0.042157010177434));
#25816=CARTESIAN_POINT('Ctrl Pts',(-1.26836088272398,-1.54298606011064,
0.0690687011598421));
#25817=CARTESIAN_POINT('Ctrl Pts',(0.609330548428412,-1.9001634242276,0.180294412497119));
#25818=CARTESIAN_POINT('Ctrl Pts',(1.92763134113508,-0.518030156334108,
0.291520123834394));
#25819=CARTESIAN_POINT('Ctrl Pts',(1.47944269002272,1.34021961655124,0.402745835171672));
#25820=CARTESIAN_POINT('Ctrl Pts',(-0.325091258553406,1.96930981947839,
0.513971546508948));
#25821=CARTESIAN_POINT('Ctrl Pts',(-1.8315117099918,0.793608534572646,0.625197257846224));
#25822=CARTESIAN_POINT('Ctrl Pts',(-1.65916676712527,-1.10972637539669,
0.7364229691835));
#25823=CARTESIAN_POINT('Ctrl Pts',(0.0340644505831978,-1.9957496809569,
0.847648680520777));
#25824=CARTESIAN_POINT('Ctrl Pts',(1.69605316295611,-1.05244701795271,0.958874391858054));
#25825=CARTESIAN_POINT('Ctrl Pts',(1.80338743872602,0.855593215941119,1.07010010319533));
#25826=CARTESIAN_POINT('Ctrl Pts',(0.257666548537818,1.97935179840939,1.18132581453261));
#25827=CARTESIAN_POINT('Ctrl Pts',(-1.52423826194019,1.28877211229984,1.29255152586988));
#25828=CARTESIAN_POINT('Ctrl Pts',(-1.90897240898426,-0.583146616891169,
1.40377723720716));
#25829=CARTESIAN_POINT('Ctrl Pts',(-0.543872574776452,-1.9205300179086,
1.51500294854444));
#25830=CARTESIAN_POINT('Ctrl Pts',(1.31976019388731,-1.49748707947159,1.62622865988171));
#25831=CARTESIAN_POINT('Ctrl Pts',(1.97365314915069,0.298207324296545,1.73745437121899));
#25832=CARTESIAN_POINT('Ctrl Pts',(0.818424019786662,1.82055379963935,1.84868008255626));
#25833=CARTESIAN_POINT('Ctrl Pts',(-1.08700216386266,1.6741148561284,1.95990579389354));
#25834=CARTESIAN_POINT('Ctrl Pts',(-1.99604281019441,-0.00687849795467773,
2.07113150523082));
#25835=CARTESIAN_POINT('Ctrl Pts',(-1.07543828510332,-1.68156672953773,
2.1823572165681));
#25836=CARTESIAN_POINT('Ctrl Pts',(0.830951927537738,-1.81486999562381,
2.29358292790537));
#25837=CARTESIAN_POINT('Ctrl Pts',(1.97566150203448,-0.284597659262374,
2.40480863924265));
#25838=CARTESIAN_POINT('Ctrl Pts',(1.30940816326546,1.50654719648941,2.51603435057992));
#25839=CARTESIAN_POINT('Ctrl Pts',(-0.557096136778581,1.91673631281949,
2.6272600619172));
#25840=CARTESIAN_POINT('Ctrl Pts',(-1.91294593480924,0.569975479650009,
2.73848577325448));
#25841=CARTESIAN_POINT('Ctrl Pts',(-1.51532018251605,-1.29924552753932,
2.84971148459175));
#25842=CARTESIAN_POINT('Ctrl Pts',(0.271302949066904,-1.97753101288966,
2.96093719592903));
#25843=CARTESIAN_POINT('Ctrl Pts',(1.80923996829539,-0.843139925493371,
3.0721629072663));
#25844=CARTESIAN_POINT('Ctrl Pts',(1.6887620836463,1.06410376450264,3.18338861860358));
#25845=CARTESIAN_POINT('Ctrl Pts',(0.0203036891799667,1.9959513914669,3.29461432994085));
#25846=CARTESIAN_POINT('Ctrl Pts',(-1.66676580240553,1.09823765951648,3.40584004127814));
#25847=CARTESIAN_POINT('Ctrl Pts',(-1.82601737245506,-0.806160500357498,
3.51706575261541));
#25848=CARTESIAN_POINT('Ctrl Pts',(-0.31147526217729,-1.97160273836024,
3.6282914639527));
#25849=CARTESIAN_POINT('Ctrl Pts',(1.48857635818734,-1.32980247507055,3.73951717528996));
#25850=CARTESIAN_POINT('Ctrl Pts',(1.92414495740429,0.530942915707476,3.85074288662724));
#25851=CARTESIAN_POINT('Ctrl Pts',(0.595972576764652,1.90500679384439,3.96196859796451));
#25852=CARTESIAN_POINT('Ctrl Pts',(-1.27848985988335,1.53287242622092,4.07319430930179));
#25853=CARTESIAN_POINT('Ctrl Pts',(-1.98104217115158,-0.244348343372923,
4.18442002063907));
#25854=CARTESIAN_POINT('Ctrl Pts',(-0.867699455103643,-1.79759056863662,
4.29564573197634));
#25855=CARTESIAN_POINT('Ctrl Pts',(1.04100801842068,-1.70309615192351,4.40687144331362));
#25856=CARTESIAN_POINT('Ctrl Pts',(1.99548982624636,-0.047482098928651,
4.5180971546509));
#25857=CARTESIAN_POINT('Ctrl Pts',(1.12083336301401,1.65165576596945,4.62932286598818));
#25858=CARTESIAN_POINT('Ctrl Pts',(-0.781219569426276,1.83682611665882,
4.74054857732545));
#25859=CARTESIAN_POINT('Ctrl Pts',(-1.96717833937204,0.338295099553305,
4.85177428866273));
#25860=CARTESIAN_POINT('Ctrl Pts',(-1.34995017532929,-1.47032946049761,
4.963));
#25861=CARTESIAN_POINT('Ctrl Pts',(0.504691233720185,-1.93119677026974,
5.07422571133729));
#25862=CARTESIAN_POINT('Ctrl Pts',(1.89671436244713,-0.621859146624829,
5.18545142267455));
#25863=CARTESIAN_POINT('Ctrl Pts',(1.55014040845374,1.25749708864148,5.29667713401184));
#25864=CARTESIAN_POINT('Ctrl Pts',(-0.217348443720809,1.98418595644765,
5.4079028453491));
#25865=CARTESIAN_POINT('Ctrl Pts',(-1.78560776525334,0.892098045178891,
5.5191285566864));
#25866=CARTESIAN_POINT('Ctrl Pts',(-1.71711445473246,-1.01771917087445,
5.63035426802365));
#25867=CARTESIAN_POINT('Ctrl Pts',(-0.0746515603857894,-1.99465828328709,
5.74157997936095));
#25868=CARTESIAN_POINT('Ctrl Pts',(1.63623915694148,-1.14322104099488,5.85280569069821));
#25869=CARTESIAN_POINT('Ctrl Pts',(1.84729473816909,0.756133444166813,5.96403140203549));
#25870=CARTESIAN_POINT('Ctrl Pts',(0.365051213003408,1.96238972900109,6.07525711337277));
#25871=CARTESIAN_POINT('Ctrl Pts',(-1.45180800902444,1.36984637716583,6.18648282471005));
#25872=CARTESIAN_POINT('Ctrl Pts',(-1.93789402341296,-0.478343766907873,
6.29770853604731));
#25873=CARTESIAN_POINT('Ctrl Pts',(-0.647623567773631,-1.88807435543072,
6.4089342473846));
#25874=CARTESIAN_POINT('Ctrl Pts',(1.23625811173359,-1.56711296880792,6.52015995872187));
#25875=CARTESIAN_POINT('Ctrl Pts',(1.98698654428125,0.190293095590063,6.63138567005915));
#25876=CARTESIAN_POINT('Ctrl Pts',(0.916284000920563,1.77332266653327,6.74261138139642));
#25877=CARTESIAN_POINT('Ctrl Pts',(-0.994151669926352,1.73075935608174,
6.8538370927337));
#25878=CARTESIAN_POINT('Ctrl Pts',(-1.99362816383988,0.101911912919242,
6.96506280407097));
#25879=CARTESIAN_POINT('Ctrl Pts',(-1.16507005656334,-1.62071885084899,
7.07628851540826));
#25880=CARTESIAN_POINT('Ctrl Pts',(0.730282785733831,-1.85703845110468,
7.18751422674552));
#25881=CARTESIAN_POINT('Ctrl Pts',(1.95844378280506,-0.392483452023516,
7.29873993808281));
#25882=CARTESIAN_POINT('Ctrl Pts',(1.38704085524538,1.43456736176966,7.40996564942008));
#25883=CARTESIAN_POINT('Ctrl Pts',(0.165022348489246,1.77169909665516,7.48411612364493));
#25884=CARTESIAN_POINT('Ctrl Pts',(-0.382243053164543,1.64449374968465,
7.52119136075736));
#25885=CARTESIAN_POINT('Ctrl Pts',(-0.802959149489926,1.63459616787395,
-0.0766913607573553));
#25886=CARTESIAN_POINT('Ctrl Pts',(-1.34693076903838,1.36738216262677,-0.0396161236449298));
#25887=CARTESIAN_POINT('Ctrl Pts',(-2.1376794572752,0.251802747388692,0.034534350579921));
#25888=CARTESIAN_POINT('Ctrl Pts',(-1.36815196105874,-1.66438387747571,
0.145760061917198));
#25889=CARTESIAN_POINT('Ctrl Pts',(0.657270967687777,-2.04966295523545,
0.256985773254474));
#25890=CARTESIAN_POINT('Ctrl Pts',(2.07929197083741,-0.558787316709069,
0.36821148459175));
#25891=CARTESIAN_POINT('Ctrl Pts',(1.59584109317654,1.44566433860368,0.479437195929027));
#25892=CARTESIAN_POINT('Ctrl Pts',(-0.350668527365547,2.12424959500892,
0.590662907266303));
#25893=CARTESIAN_POINT('Ctrl Pts',(-1.97560991659234,0.856047429148608,
0.70188861860358));
#25894=CARTESIAN_POINT('Ctrl Pts',(-1.7897053567994,-1.1970365354353,0.813114329940855));
#25895=CARTESIAN_POINT('Ctrl Pts',(0.0367445460535571,-2.15276967066298,
0.924340041278132));
#25896=CARTESIAN_POINT('Ctrl Pts',(1.8294938708412,-1.13525059873339,1.03556575261541));
#25897=CARTESIAN_POINT('Ctrl Pts',(1.94527290651128,0.922908891469747,1.14679146395268));
#25898=CARTESIAN_POINT('Ctrl Pts',(0.277939030194749,2.13508164868898,1.25801717528996));
#25899=CARTESIAN_POINT('Ctrl Pts',(-1.64416105510567,1.39016908895364,1.36924288662724));
#25900=CARTESIAN_POINT('Ctrl Pts',(-2.05916500621629,-0.629026957825243,
1.48046859796451));
#25901=CARTESIAN_POINT('Ctrl Pts',(-0.586662944183848,-2.07163193540842,
1.59169430930179));
#25902=CARTESIAN_POINT('Ctrl Pts',(1.42359522592366,-1.61530516459883,1.70292002063907));
#25903=CARTESIAN_POINT('Ctrl Pts',(2.12893464568308,0.32166944053191,1.81414573197634));
#25904=CARTESIAN_POINT('Ctrl Pts',(0.882815327167714,1.96378986857444,1.92537144331362));
#25905=CARTESIAN_POINT('Ctrl Pts',(-1.17252444664632,1.80582951953752,2.0365971546509));
#25906=CARTESIAN_POINT('Ctrl Pts',(-2.1530858624871,-0.00741967888950297,
2.14782286598817));
#25907=CARTESIAN_POINT('Ctrl Pts',(-1.16005075432617,-1.81386768545496,
2.25904857732545));
#25908=CARTESIAN_POINT('Ctrl Pts',(0.896328895577965,-1.95765887879382,
2.37027428866273));
#25909=CARTESIAN_POINT('Ctrl Pts',(2.13110101014124,-0.306989005208296,
2.4815));
#25910=CARTESIAN_POINT('Ctrl Pts',(1.41242872655496,1.62507810622307,2.59272571133728));
#25911=CARTESIAN_POINT('Ctrl Pts',(-0.600926898971321,2.06753975223876,
2.70395142267456));
#25912=CARTESIAN_POINT('Ctrl Pts',(-2.06345115791318,0.614819552431958,
2.81517713401183));
#25913=CARTESIAN_POINT('Ctrl Pts',(-1.63454132619476,-1.40146652314137,
2.92640284534911));
#25914=CARTESIAN_POINT('Ctrl Pts',(0.292648304487066,-2.13311760886924,
3.03762855668638));
#25915=CARTESIAN_POINT('Ctrl Pts',(1.95158589669928,-0.909475811043054,
3.14885426802366));
#25916=CARTESIAN_POINT('Ctrl Pts',(1.82162914985223,1.14782446542155,3.26007997936093));
#25917=CARTESIAN_POINT('Ctrl Pts',(0.021901126522171,2.15298725119041,3.37130569069822));
#25918=CARTESIAN_POINT('Ctrl Pts',(-1.79790226287119,1.18464391959888,3.48253140203548));
#25919=CARTESIAN_POINT('Ctrl Pts',(-1.96968329998188,-0.869586948411284,
3.59375711337277));
#25920=CARTESIAN_POINT('Ctrl Pts',(-0.335981262567754,-2.12672291432008,
3.70498282471004));
#25921=CARTESIAN_POINT('Ctrl Pts',(1.60569337274561,-1.43442760563632,3.81620853604732));
#25922=CARTESIAN_POINT('Ctrl Pts',(2.07553128820896,0.572716015788303,3.9274342473846));
#25923=CARTESIAN_POINT('Ctrl Pts',(0.642862028263319,2.05488738759502,4.03865995872187));
#25924=CARTESIAN_POINT('Ctrl Pts',(-1.37907785774386,1.65347453122567,4.14988567005915));
#25925=CARTESIAN_POINT('Ctrl Pts',(-2.13690501521948,-0.263572985985768,
4.26111138139642));
#25926=CARTESIAN_POINT('Ctrl Pts',(-0.935967615589101,-1.93901995493508,
4.3723370927337));
#25927=CARTESIAN_POINT('Ctrl Pts',(1.12291161078803,-1.83709098243517,4.48356280407097));
#25928=CARTESIAN_POINT('Ctrl Pts',(2.15248937131234,-0.0512178573537473,
4.59478851540826));
#25929=CARTESIAN_POINT('Ctrl Pts',(1.20901738969933,1.78160341113012,4.70601422674553));
#25930=CARTESIAN_POINT('Ctrl Pts',(-0.842683734957634,1.9813424458767,4.81723993808281));
#25931=CARTESIAN_POINT('Ctrl Pts',(-2.12195041602352,0.364911209557656,
4.92846564942008));
#25932=CARTESIAN_POINT('Ctrl Pts',(-1.45616047046626,-1.58601086030181,
5.03969136075736));
#25933=CARTESIAN_POINT('Ctrl Pts',(0.544398925060255,-2.08313791794051,
5.15091707209464));
#25934=CARTESIAN_POINT('Ctrl Pts',(2.04594253094371,-0.670785280865706,
5.26214278343191));
#25935=CARTESIAN_POINT('Ctrl Pts',(1.67210110988885,1.35643343411504,5.37336849476919));
#25936=CARTESIAN_POINT('Ctrl Pts',(-0.234448809924699,2.14029614472887,
5.48459420610646));
#25937=CARTESIAN_POINT('Ctrl Pts',(-1.92609437817603,0.96228581832871,5.59581991744374));
#25938=CARTESIAN_POINT('Ctrl Pts',(-1.85221220600806,-1.09779046200839,
5.70704562878101));
#25939=CARTESIAN_POINT('Ctrl Pts',(-0.0805249358672843,-2.15159240488431,
5.8182713401183));
#25940=CARTESIAN_POINT('Ctrl Pts',(1.76497386652513,-1.23316646741867,5.92949705145556));
#25941=CARTESIAN_POINT('Ctrl Pts',(1.99263470917806,0.815623903693059,6.04072276279285));
#25942=CARTESIAN_POINT('Ctrl Pts',(0.393772419001808,2.11678505121371,6.15194847413012));
#25943=CARTESIAN_POINT('Ctrl Pts',(-1.56603219295262,1.47762204968323,6.2631741854674));
#25944=CARTESIAN_POINT('Ctrl Pts',(-2.09036209218494,-0.515978513425692,
6.37439989680467));
#25945=CARTESIAN_POINT('Ctrl Pts',(-0.698576774438554,-2.03662275239797,
6.48562560814195));
#25946=CARTESIAN_POINT('Ctrl Pts',(1.33352343404865,-1.69040902370822,6.59685131947923));
#25947=CARTESIAN_POINT('Ctrl Pts',(2.14331707496162,0.205264822854154,6.70807703081651));
#25948=CARTESIAN_POINT('Ctrl Pts',(0.988374657261507,1.9128427223306,6.81930274215378));
#25949=CARTESIAN_POINT('Ctrl Pts',(-1.07236873615846,1.86693064994129,6.93052845349106));
#25950=CARTESIAN_POINT('Ctrl Pts',(-2.15048123852699,0.109930056512203,
7.04175416482834));
#25951=CARTESIAN_POINT('Ctrl Pts',(-1.25673450227717,-1.74823246626129,
7.1529798761656));
#25952=CARTESIAN_POINT('Ctrl Pts',(0.787739387928281,-2.00314503013039,
7.26420558750289));
#25953=CARTESIAN_POINT('Ctrl Pts',(2.11252864903365,-0.42336294968026,7.37543129884016));
#25954=CARTESIAN_POINT('Ctrl Pts',(1.49616934109244,1.54743509990691,7.48665701017744));
#25955=CARTESIAN_POINT('Ctrl Pts',(0.178005844219355,1.91109141452625,7.56080748440229));
#25956=CARTESIAN_POINT('Ctrl Pts',(-0.412316864948557,1.77387790748314,
7.59788272151472));
#25957=CARTESIAN_POINT('Ctrl Pts',(-0.861525859670525,1.75382131162755,
0.));
#25958=CARTESIAN_POINT('Ctrl Pts',(-1.44517400349647,1.4671170929474,0.0370752371124254));
#25959=CARTESIAN_POINT('Ctrl Pts',(-2.29359878805659,0.270168885365161,
0.111225711337276));
#25960=CARTESIAN_POINT('Ctrl Pts',(-1.46794303939349,-1.78578169484077,
0.222451422674553));
#25961=CARTESIAN_POINT('Ctrl Pts',(0.705211386947141,-2.19916248624329,
0.33367713401183));
#25962=CARTESIAN_POINT('Ctrl Pts',(2.23095260053975,-0.599544477084032,
0.444902845349104));
#25963=CARTESIAN_POINT('Ctrl Pts',(1.71223949633035,1.55110906065613,0.556128556686383));
#25964=CARTESIAN_POINT('Ctrl Pts',(-0.376245796177686,2.27918937053945,
0.667354268023658));
#25965=CARTESIAN_POINT('Ctrl Pts',(-2.11970812319287,0.918486323724569,
0.778579979360935));
#25966=CARTESIAN_POINT('Ctrl Pts',(-1.92024394647352,-1.28434669547391,
0.889805690698211));
#25967=CARTESIAN_POINT('Ctrl Pts',(0.0394246415239131,-2.30978966036907,
1.00103140203549));
#25968=CARTESIAN_POINT('Ctrl Pts',(1.96293457872629,-1.21805417951409,1.11225711337277));
#25969=CARTESIAN_POINT('Ctrl Pts',(2.08715837429654,0.990224566998375,1.22348282471004));
#25970=CARTESIAN_POINT('Ctrl Pts',(0.298211511851683,2.29081149896857,1.33470853604732));
#25971=CARTESIAN_POINT('Ctrl Pts',(-1.76408384827114,1.49156606560744,1.44593424738459));
#25972=CARTESIAN_POINT('Ctrl Pts',(-2.20935760344832,-0.674907298759319,
1.55715995872187));
#25973=CARTESIAN_POINT('Ctrl Pts',(-0.629453313591242,-2.22273385290824,
1.66838567005915));
#25974=CARTESIAN_POINT('Ctrl Pts',(1.52743025795999,-1.73312324972607,1.77961138139642));
#25975=CARTESIAN_POINT('Ctrl Pts',(2.28421614221547,0.345131556767278,1.8908370927337));
#25976=CARTESIAN_POINT('Ctrl Pts',(0.947206634548765,2.10702593750954,2.00206280407097));
#25977=CARTESIAN_POINT('Ctrl Pts',(-1.25804672942998,1.93754418294664,2.11328851540825));
#25978=CARTESIAN_POINT('Ctrl Pts',(-2.31012891477979,-0.0079608598243287,
2.22451422674552));
#25979=CARTESIAN_POINT('Ctrl Pts',(-1.24466322354901,-1.94616864137219,
2.33573993808281));
#25980=CARTESIAN_POINT('Ctrl Pts',(0.961705863618192,-2.10044776196383,
2.44696564942008));
#25981=CARTESIAN_POINT('Ctrl Pts',(2.286540518248,-0.329380351154219,2.55819136075736));
#25982=CARTESIAN_POINT('Ctrl Pts',(1.51544928984446,1.74360901595674,2.66941707209463));
#25983=CARTESIAN_POINT('Ctrl Pts',(-0.644757661164061,2.21834319165802,
2.78064278343191));
#25984=CARTESIAN_POINT('Ctrl Pts',(-2.21395638101712,0.659663625213907,
2.89186849476918));
#25985=CARTESIAN_POINT('Ctrl Pts',(-1.75376246987347,-1.50368751874342,
3.00309420610647));
#25986=CARTESIAN_POINT('Ctrl Pts',(0.313993659907229,-2.28870420484881,
3.11431991744373));
#25987=CARTESIAN_POINT('Ctrl Pts',(2.09393182510317,-0.975811696592738,
3.22554562878102));
#25988=CARTESIAN_POINT('Ctrl Pts',(1.95449621605817,1.23154516634045,3.33677134011829));
#25989=CARTESIAN_POINT('Ctrl Pts',(0.0234985638643735,2.31002311091391,
3.44799705145557));
#25990=CARTESIAN_POINT('Ctrl Pts',(-1.92903872333685,1.27105017968128,3.55922276279284));
#25991=CARTESIAN_POINT('Ctrl Pts',(-2.1133492275087,-0.93301339646507,3.67044847413012));
#25992=CARTESIAN_POINT('Ctrl Pts',(-0.360487262958215,-2.28184309027991,
3.7816741854674));
#25993=CARTESIAN_POINT('Ctrl Pts',(1.72281038730387,-1.53905273620209,3.89289989680467));
#25994=CARTESIAN_POINT('Ctrl Pts',(2.22691761901362,0.614489115869131,4.00412560814195));
#25995=CARTESIAN_POINT('Ctrl Pts',(0.689751479761988,2.20476798134566,4.11535131947922));
#25996=CARTESIAN_POINT('Ctrl Pts',(-1.47966585560437,1.77407663623043,4.22657703081651));
#25997=CARTESIAN_POINT('Ctrl Pts',(-2.29276785928738,-0.282797628598616,
4.33780274215377));
#25998=CARTESIAN_POINT('Ctrl Pts',(-1.00423577607456,-2.08044934123353,
4.44902845349105));
#25999=CARTESIAN_POINT('Ctrl Pts',(1.20481520315537,-1.97108581294683,4.56025416482834));
#26000=CARTESIAN_POINT('Ctrl Pts',(2.30948891637831,-0.0549536157788429,
4.6714798761656));
#26001=CARTESIAN_POINT('Ctrl Pts',(1.29720141638464,1.91155105629079,4.78270558750289));
#26002=CARTESIAN_POINT('Ctrl Pts',(-0.904147900488994,2.12585877509457,
4.89393129884016));
#26003=CARTESIAN_POINT('Ctrl Pts',(-2.276722492675,0.391527319562006,5.00515701017744));
#26004=CARTESIAN_POINT('Ctrl Pts',(-1.56237076560323,-1.701692260106,5.11638272151471));
#26005=CARTESIAN_POINT('Ctrl Pts',(0.584106616400323,-2.2350790656113,5.227608432852));
#26006=CARTESIAN_POINT('Ctrl Pts',(2.19517069944029,-0.71971141510658,5.33883414418926));
#26007=CARTESIAN_POINT('Ctrl Pts',(1.79406181132396,1.4553697795886,5.45005985552654));
#26008=CARTESIAN_POINT('Ctrl Pts',(-0.251549176128587,2.2964063330101,5.56128556686382));
#26009=CARTESIAN_POINT('Ctrl Pts',(-2.06658099109872,1.03247359147853,5.6725112782011));
#26010=CARTESIAN_POINT('Ctrl Pts',(-1.98730995728366,-1.17786175314234,
5.78373698953836));
#26011=CARTESIAN_POINT('Ctrl Pts',(-0.0863983113487825,-2.30852652648153,
5.89496270087566));
#26012=CARTESIAN_POINT('Ctrl Pts',(1.89370857610877,-1.32311189384246,6.00618841221292));
#26013=CARTESIAN_POINT('Ctrl Pts',(2.13797468018702,0.875114363219305,6.1174141235502));
#26014=CARTESIAN_POINT('Ctrl Pts',(0.422493625000208,2.27118037342633,6.22863983488748));
#26015=CARTESIAN_POINT('Ctrl Pts',(-1.68025637688079,1.58539772220062,6.33986554622475));
#26016=CARTESIAN_POINT('Ctrl Pts',(-2.24283016095692,-0.55361325994351,
6.45109125756204));
#26017=CARTESIAN_POINT('Ctrl Pts',(-0.749529981103475,-2.18517114936522,
6.56231696889931));
#26018=CARTESIAN_POINT('Ctrl Pts',(1.43078875636371,-1.81370507860851,6.67354268023658));
#26019=CARTESIAN_POINT('Ctrl Pts',(2.29964760564199,0.22023655011824,6.78476839157387));
#26020=CARTESIAN_POINT('Ctrl Pts',(1.06046531360245,2.05236277812793,6.89599410291113));
#26021=CARTESIAN_POINT('Ctrl Pts',(-1.15058580239056,2.00310194380083,7.00721981424842));
#26022=CARTESIAN_POINT('Ctrl Pts',(-2.30733431321409,0.117948200105168,
7.11844552558569));
#26023=CARTESIAN_POINT('Ctrl Pts',(-1.34839894799099,-1.87574608167359,
7.22967123692297));
#26024=CARTESIAN_POINT('Ctrl Pts',(0.845195990122731,-2.1492516091561,7.34089694826023));
#26025=CARTESIAN_POINT('Ctrl Pts',(2.26661351526224,-0.454242447337005,
7.45212265959753));
#26026=CARTESIAN_POINT('Ctrl Pts',(1.60529782693949,1.66030283804416,7.56334837093479));
#26027=CARTESIAN_POINT('Ctrl Pts',(0.190989339949464,2.05048373239734,7.63749884515964));
#26028=CARTESIAN_POINT('Ctrl Pts',(-0.442390676732572,1.90326206528163,
7.67457408227207));
#26029=CARTESIAN_POINT('Ctrl Pts',(-1.95381346134878,-0.0017935399644829,
6.42413030787577));
#26030=CARTESIAN_POINT('Ctrl Pts',(-1.9552538907035,-0.159408210813097,
6.43311729110453));
#26031=CARTESIAN_POINT('Ctrl Pts',(-1.93778561972322,-0.316707681574419,
6.44210427433328));
#26032=CARTESIAN_POINT('Ctrl Pts',(-1.90018450030199,-0.469037744489771,
6.45109125756203));
#26033=CARTESIAN_POINT('Ctrl Pts',(-1.7450634343391,-1.09746588975075,6.48816649467446));
#26034=CARTESIAN_POINT('Ctrl Pts',(-1.24729670772129,-1.64131851955799,
6.52524173178688));
#26035=CARTESIAN_POINT('Ctrl Pts',(-0.635026888167849,-1.85133382266882,
6.56231696889931));
#26036=CARTESIAN_POINT('Ctrl Pts',(-0.02275706861441,-2.06134912577965,
6.59939220601173));
#26037=CARTESIAN_POINT('Ctrl Pts',(0.704015843874659,-1.93752710219408,
6.63646744312416));
#26038=CARTESIAN_POINT('Ctrl Pts',(1.21221210833224,-1.53662581894683,6.67354268023658));
#26039=CARTESIAN_POINT('Ctrl Pts',(1.7204083727898,-1.1357245356996,6.71061791734901));
#26040=CARTESIAN_POINT('Ctrl Pts',(2.01002798921589,-0.457743992790703,
6.74769315446144));
#26041=CARTESIAN_POINT('Ctrl Pts',(1.94830741542236,0.186600649998693,6.78476839157386));
#26042=CARTESIAN_POINT('Ctrl Pts',(1.88658684162883,0.830945292788112,6.82184362868628));
#26043=CARTESIAN_POINT('Ctrl Pts',(1.47352607761564,1.44165403545803,6.85891886579871));
#26044=CARTESIAN_POINT('Ctrl Pts',(0.898487176276873,1.73879826773846,6.89599410291113));
#26045=CARTESIAN_POINT('Ctrl Pts',(0.323448274938114,2.0359425000189,6.93306934002356));
#26046=CARTESIAN_POINT('Ctrl Pts',(-0.413568763726226,2.01952222190986,
6.97014457713599));
#26047=CARTESIAN_POINT('Ctrl Pts',(-0.974868701528982,1.69711979223941,
7.00721981424841));
#26048=CARTESIAN_POINT('Ctrl Pts',(-1.17057269468519,1.58471029663753,7.02014654283228));
#26049=CARTESIAN_POINT('Ctrl Pts',(-1.344915597571,1.43510400955329,7.03307327141614));
#26050=CARTESIAN_POINT('Ctrl Pts',(-1.49039960333529,1.260503289177,7.046));
#26051=CARTESIAN_POINT('Ctrl Pts',(-0.905552056217064,-1.26793026328003,
2.94902990916057E-17));
#26052=CARTESIAN_POINT('Ctrl Pts',(-0.937134822631023,-1.25104249355971,
4.75162406228688E-17));
#26053=CARTESIAN_POINT('Ctrl Pts',(-0.968036761240596,-1.23301924856148,
-1.58634398933136E-16));
#26054=CARTESIAN_POINT('Ctrl Pts',(-0.998189477963827,-1.21387418528302,
-1.99493199737333E-16));
#26055=CARTESIAN_POINT('Ctrl Pts',(-1.04824220989901,-1.18209387411058,
-2.7512401071258E-16));
#26056=CARTESIAN_POINT('Ctrl Pts',(-1.09623172292828,-1.14722531738451,
-1.13947733410607E-16));
#26057=CARTESIAN_POINT('Ctrl Pts',(-1.14207949782356,-1.10958932626875,
-2.28983498828939E-16));
#26058=CARTESIAN_POINT('Ctrl Pts',(-1.16812476791348,-1.08820901815237,
-2.94333182366767E-16));
#26059=CARTESIAN_POINT('Ctrl Pts',(-1.19347860393222,-1.06593466358557,
-2.59231987339497E-16));
#26060=CARTESIAN_POINT('Ctrl Pts',(-1.21812392229353,-1.04281835170969,
-2.1163626406917E-16));
#26061=CARTESIAN_POINT('Ctrl Pts',(-1.23207453972119,-1.02973323677667,
-1.84694444255666E-16));
#26062=CARTESIAN_POINT('Ctrl Pts',(-1.24580226168736,-1.01637377846959,
3.24804729171387E-17));
#26063=CARTESIAN_POINT('Ctrl Pts',(-1.2592797890629,-1.00277371885107,1.38777878078145E-17));
#26064=CARTESIAN_POINT('Ctrl Pts',(-1.30315654392119,-0.95849805423447,
-4.66841707402696E-17));
#26065=CARTESIAN_POINT('Ctrl Pts',(-1.34442524303116,-0.911639949761556,
-4.44200463634023E-16));
#26066=CARTESIAN_POINT('Ctrl Pts',(-1.38299703120573,-0.862548384977714,
-4.09394740330526E-16));
#26067=CARTESIAN_POINT('Ctrl Pts',(-1.41261207961662,-0.824856353147081,
-3.82671240347992E-16));
#26068=CARTESIAN_POINT('Ctrl Pts',(-1.44063702556457,-0.785846462927244,
-3.12176496943412E-16));
#26069=CARTESIAN_POINT('Ctrl Pts',(-1.46702161869435,-0.745658482546257,
-3.67761376907083E-16));
#26070=CARTESIAN_POINT('Ctrl Pts',(-1.48012065014873,-0.725706550124602,
-3.9535733366299E-16));
#26071=CARTESIAN_POINT('Ctrl Pts',(-1.4928152185087,-0.705464023789787,
-1.55640291167757E-16));
#26072=CARTESIAN_POINT('Ctrl Pts',(-1.50509817356396,-0.68494682789941,
-1.17961196366423E-16));
#26073=CARTESIAN_POINT('Ctrl Pts',(-1.5112932288107,-0.674598734832467,
-9.89572943826601E-17));
#26074=CARTESIAN_POINT('Ctrl Pts',(-1.51737856906155,-0.664189090325049,
-2.93080070452884E-16));
#26075=CARTESIAN_POINT('Ctrl Pts',(-1.52335311621856,-0.653721302282831,
-2.77555756156289E-16));
#26076=CARTESIAN_POINT('Ctrl Pts',(-1.55547318924941,-0.597444883744102,
-1.94094684403748E-16));
#26077=CARTESIAN_POINT('Ctrl Pts',(-1.58439860819566,-0.539482552118629,
-3.31420483543467E-16));
#26078=CARTESIAN_POINT('Ctrl Pts',(-1.61003533926912,-0.480187572841947,
-3.19189119579733E-16));
#26079=CARTESIAN_POINT('Ctrl Pts',(-1.63616747730804,-0.419746770969312,
-3.06721395415186E-16));
#26080=CARTESIAN_POINT('Ctrl Pts',(-1.65888335052524,-0.357920523309995,
-2.80209762252872E-16));
#26081=CARTESIAN_POINT('Ctrl Pts',(-1.67804895967927,-0.295042072125015,
-1.66533453693773E-16));
#26082=CARTESIAN_POINT('Ctrl Pts',(-1.69039160882678,-0.254548359888778,
-9.33259296514283E-17));
#26083=CARTESIAN_POINT('Ctrl Pts',(-1.70126111007635,-0.213617460141972,
-2.30505991696603E-16));
#26084=CARTESIAN_POINT('Ctrl Pts',(-1.71061208520917,-0.172332131165316,
-2.91433543964104E-16));
#26085=CARTESIAN_POINT('Ctrl Pts',(-1.715816487101,-0.149354266164202,-3.2534353343379E-16));
#26086=CARTESIAN_POINT('Ctrl Pts',(-1.72055036402814,-0.126266539334649,
-1.00298932279788E-16));
#26087=CARTESIAN_POINT('Ctrl Pts',(-1.72480472543126,-0.103082789841687,
-9.71445146547012E-17));
#26088=CARTESIAN_POINT('Ctrl Pts',(-1.72695538876364,-0.0913629486676286,
-9.55498945276206E-17));
#26089=CARTESIAN_POINT('Ctrl Pts',(-1.72898375858757,-0.07961694527504,
-1.96680959500023E-16));
#26090=CARTESIAN_POINT('Ctrl Pts',(-1.73088777000182,-0.0678516147389183,
-1.94289029309402E-16));
#26091=CARTESIAN_POINT('Ctrl Pts',(-1.74172080812434,-0.000911745960731708,
-1.80679934979654E-16));
#26092=CARTESIAN_POINT('Ctrl Pts',(-1.74848760095285,0.0663732156671881,
-2.27318435210151E-17));
#26093=CARTESIAN_POINT('Ctrl Pts',(-1.75106859893149,0.133645381706535,
-4.16333634234434E-17));
#26094=CARTESIAN_POINT('Ctrl Pts',(-1.75197360252239,0.157233758116401,
-4.82610103750263E-17));
#26095=CARTESIAN_POINT('Ctrl Pts',(-1.75236359562623,0.180820850215305,
-8.28170566717793E-17));
#26096=CARTESIAN_POINT('Ctrl Pts',(-1.75223214201128,0.204392038445102,
-5.55111512312578E-17));
#26097=CARTESIAN_POINT('Ctrl Pts',(-1.75187057279805,0.269225675666801,
2.10533692500149E-17));
#26098=CARTESIAN_POINT('Ctrl Pts',(-1.74756789056806,0.333938320850628,
-1.60420900056E-17));
#26099=CARTESIAN_POINT('Ctrl Pts',(-1.73954116331082,0.398294466418659,
0.));
#26100=CARTESIAN_POINT('Ctrl Pts',(-1.73091740426649,0.467437452671242,
1.72353082822116E-17));
#26101=CARTESIAN_POINT('Ctrl Pts',(-1.71799540177027,0.536169874708505,
-4.36478159584899E-17));
#26102=CARTESIAN_POINT('Ctrl Pts',(-1.70098034075862,0.604204029641736,
8.32667268468867E-17));
#26103=CARTESIAN_POINT('Ctrl Pts',(-1.69824130486499,0.615155973465351,
1.03697067233541E-16));
#26104=CARTESIAN_POINT('Ctrl Pts',(-1.69539827041295,0.626080961021427,
1.29813171089747E-16));
#26105=CARTESIAN_POINT('Ctrl Pts',(-1.69245305315959,0.636975805303662,
1.11022302462516E-16));
#26106=CARTESIAN_POINT('Ctrl Pts',(-1.67473398681781,0.702521553550295,
-2.02764230671151E-18));
#26107=CARTESIAN_POINT('Ctrl Pts',(-1.65331496860816,0.766998932259627,
-2.57263159617093E-16));
#26108=CARTESIAN_POINT('Ctrl Pts',(-1.62845169327078,0.83015154980978,-1.94289029309402E-16));
#26109=CARTESIAN_POINT('Ctrl Pts',(-1.60307671281799,0.894603896257815,
-1.30018843507023E-16));
#26110=CARTESIAN_POINT('Ctrl Pts',(-1.57411406965586,0.957677277748301,
-1.42237185085071E-16));
#26111=CARTESIAN_POINT('Ctrl Pts',(-1.54178048300264,1.01910167818773,-5.55111512312578E-17));
#26112=CARTESIAN_POINT('Ctrl Pts',(-1.50922784853364,1.08094220569947,3.18024186880875E-17));
#26113=CARTESIAN_POINT('Ctrl Pts',(-1.47325811155629,1.14111231916335,-1.86023089836484E-16));
#26114=CARTESIAN_POINT('Ctrl Pts',(-1.43404118681899,1.19932479720781,-1.66533453693773E-16));
#26115=CARTESIAN_POINT('Ctrl Pts',(-1.42513259519695,1.21254845504633,-1.62106150675484E-16));
#26116=CARTESIAN_POINT('Ctrl Pts',(-1.41605624454103,1.22567101155683,-3.77067070771252E-16));
#26117=CARTESIAN_POINT('Ctrl Pts',(-1.40681378949184,1.23868893327645,-3.88578058618805E-16));
#26118=CARTESIAN_POINT('Ctrl Pts',(-1.40005105796202,1.24821418486786,-3.97000682266051E-16));
#26119=CARTESIAN_POINT('Ctrl Pts',(-1.39319940015811,1.25768325768832,-4.06719094166719E-16));
#26120=CARTESIAN_POINT('Ctrl Pts',(-1.3862680939899,1.26708342641975,-3.88578058618805E-16));
#26121=CARTESIAN_POINT('Ctrl Pts',(-1.34342259960335,1.32519006127916,-2.76440228046676E-16));
#26122=CARTESIAN_POINT('Ctrl Pts',(-1.2974598126633,1.38077597290076,-1.69458509682717E-16));
#26123=CARTESIAN_POINT('Ctrl Pts',(-1.24862081372783,1.43356038861728,-1.94289029309402E-16));
#26124=CARTESIAN_POINT('Ctrl Pts',(-1.19966911793571,1.48646660530969,-2.19176845800727E-16));
#26125=CARTESIAN_POINT('Ctrl Pts',(-1.14782748930566,1.53655939185262,-1.74330404157582E-16));
#26126=CARTESIAN_POINT('Ctrl Pts',(-1.09328907277386,1.5835398262669,-5.55111512312578E-17));
#26127=CARTESIAN_POINT('Ctrl Pts',(-1.03991703070208,1.62951552342795,6.07669985463979E-17));
#26128=CARTESIAN_POINT('Ctrl Pts',(-0.983961746585148,1.67251142482066,
1.56834561468643E-16));
#26129=CARTESIAN_POINT('Ctrl Pts',(-0.925564466602708,1.71221823957964,
2.22044604925031E-16));
#26130=CARTESIAN_POINT('Ctrl Pts',(-0.904533489913129,1.72651810244765,
2.45529104618684E-16));
#26131=CARTESIAN_POINT('Ctrl Pts',(-0.883185451447723,1.74039103644132,
-1.04689938393391E-17));
#26132=CARTESIAN_POINT('Ctrl Pts',(-0.861525859670525,1.75382131162755,
0.));
#26133=CARTESIAN_POINT('Origin',(0.,0.,0.));
#26134=CARTESIAN_POINT('Origin',(-0.866025403784439,-1.5,-4.));
#26135=CARTESIAN_POINT('',(-0.866025403784439,-1.5,-4.));
#26136=CARTESIAN_POINT('',(0.866025403784439,-1.5,-4.));
#26137=CARTESIAN_POINT('',(-0.43301270189222,-1.5,-4.));
#26138=CARTESIAN_POINT('',(-0.866025403784439,-1.5,-2.));
#26139=CARTESIAN_POINT('',(-0.866025403784439,-1.5,-4.));
#26140=CARTESIAN_POINT('',(0.866025403784439,-1.5,-2.));
#26141=CARTESIAN_POINT('',(-0.866025403784439,-1.5,-2.));
#26142=CARTESIAN_POINT('',(0.866025403784439,-1.5,-4.));
#26143=CARTESIAN_POINT('Origin',(-1.73205080756888,2.12115047744981E-16,
-4.));
#26144=CARTESIAN_POINT('',(-1.73205080756888,2.12115047744981E-16,-4.));
#26145=CARTESIAN_POINT('',(-1.51554445662277,-0.375,-4.));
#26146=CARTESIAN_POINT('',(-1.73205080756888,2.77555756156289E-16,-2.));
#26147=CARTESIAN_POINT('',(-1.73205080756888,2.12115047744981E-16,-4.));
#26148=CARTESIAN_POINT('',(-1.73205080756888,2.12115047744981E-16,-2.));
#26149=CARTESIAN_POINT('Origin',(-0.866025403784438,1.5,-4.));
#26150=CARTESIAN_POINT('',(-0.866025403784438,1.5,-4.));
#26151=CARTESIAN_POINT('',(-1.08253175473055,1.125,-4.));
#26152=CARTESIAN_POINT('',(-0.866025403784438,1.5,-2.));
#26153=CARTESIAN_POINT('',(-0.866025403784438,1.5,-4.));
#26154=CARTESIAN_POINT('',(-0.866025403784438,1.5,-2.));
#26155=CARTESIAN_POINT('Origin',(0.866025403784439,1.5,-4.));
#26156=CARTESIAN_POINT('',(0.866025403784439,1.5,-4.));
#26157=CARTESIAN_POINT('',(0.43301270189222,1.5,-4.));
#26158=CARTESIAN_POINT('',(0.866025403784439,1.5,-2.));
#26159=CARTESIAN_POINT('',(0.866025403784439,1.5,-4.));
#26160=CARTESIAN_POINT('',(0.866025403784439,1.5,-2.));
#26161=CARTESIAN_POINT('Origin',(1.73205080756888,0.,-4.));
#26162=CARTESIAN_POINT('',(1.73205080756888,0.,-4.));
#26163=CARTESIAN_POINT('',(1.51554445662277,0.375,-4.));
#26164=CARTESIAN_POINT('',(1.73205080756888,0.,-2.));
#26165=CARTESIAN_POINT('',(1.73205080756888,0.,-4.));
#26166=CARTESIAN_POINT('',(1.73205080756888,0.,-2.));
#26167=CARTESIAN_POINT('Origin',(0.866025403784439,-1.5,-4.));
#26168=CARTESIAN_POINT('',(1.08253175473055,-1.125,-4.));
#26169=CARTESIAN_POINT('',(0.866025403784439,-1.5,-2.));
#26170=CARTESIAN_POINT('Origin',(0.,2.77555756156289E-16,-2.));
#26171=CARTESIAN_POINT('Origin',(0.,0.,0.));
#26172=CARTESIAN_POINT('',(-3.5,-4.28626379701574E-16,0.));
#26173=CARTESIAN_POINT('Origin',(0.,0.,0.));
#26174=CARTESIAN_POINT('Origin',(0.,0.,-4.));
#26175=CARTESIAN_POINT('',(-3.5,-4.28626379701574E-16,-4.));
#26176=CARTESIAN_POINT('',(-3.5,-4.28626379701574E-16,-4.));
#26177=CARTESIAN_POINT('Origin',(0.,0.,-4.));
#26178=CARTESIAN_POINT('Origin',(0.,0.,-4.));
#26179=CARTESIAN_POINT('Origin',(0.,0.,8.));
#32597=UNCERTAINTY_MEASURE_WITH_UNIT(LENGTH_MEASURE(0.01),#32628,
'DISTANCE_ACCURACY_VALUE',
'Maximum model space distance between geometric entities at asserted c
onnectivities');
#32607=UNCERTAINTY_MEASURE_WITH_UNIT(LENGTH_MEASURE(0.01),#32628,
'DISTANCE_ACCURACY_VALUE',
'Maximum model space distance between geometric entities at asserted c
onnectivities');
#32617=(
GEOMETRIC_REPRESENTATION_CONTEXT(3)
GLOBAL_UNCERTAINTY_ASSIGNED_CONTEXT((#32597))
GLOBAL_UNIT_ASSIGNED_CONTEXT((#32628,#32630,#32631))
REPRESENTATION_CONTEXT('','3D')
);
#32627=(
GEOMETRIC_REPRESENTATION_CONTEXT(3)
GLOBAL_UNCERTAINTY_ASSIGNED_CONTEXT((#32607))
GLOBAL_UNIT_ASSIGNED_CONTEXT((#32628,#32630,#32631))
REPRESENTATION_CONTEXT('','3D')
);
#32628=(
LENGTH_UNIT()
NAMED_UNIT(*)
SI_UNIT(.MILLI.,.METRE.)
);
#32630=(
NAMED_UNIT(*)
PLANE_ANGLE_UNIT()
SI_UNIT($,.RADIAN.)
);
#32631=(
NAMED_UNIT(*)
SI_UNIT($,.STERADIAN.)
SOLID_ANGLE_UNIT()
);
#32641=SHAPE_DEFINITION_REPRESENTATION(#32660,#32716);
#32660=PRODUCT_DEFINITION_SHAPE('',$,#32736);
#32716=SHAPE_REPRESENTATION('',(#9225),#32617);
#32726=PRODUCT_DEFINITION_CONTEXT('part definition',#32785,'design');
#32736=PRODUCT_DEFINITION('Socket head cap screw M4x8',
'Socket head cap screw M4x8',#32755,#32726);
#32755=PRODUCT_DEFINITION_FORMATION('',$,#32796);
#32785=APPLICATION_CONTEXT(
'Core Data for Automotive Mechanical Design Process');
#32786=PRODUCT_CONTEXT('part definition',#32785,'mechanical');
#32796=PRODUCT('Socket head cap screw M4x8',
'Socket head cap screw M4x8',$,(#32786));
#32809=PRESENTATION_STYLE_ASSIGNMENT((#32816));
#32816=SURFACE_STYLE_USAGE(.BOTH.,#32823);
#32823=SURFACE_SIDE_STYLE('',(#32830));
#32830=SURFACE_STYLE_FILL_AREA(#32837);
#32837=FILL_AREA_STYLE('Dark gray',(#32844));
#32844=FILL_AREA_STYLE_COLOUR('Dark gray',#32851);
#32851=COLOUR_RGB('Dark gray',0.250980392156863,0.282352941176471,0.32156862745098);
ENDSEC;
END-ISO-10303-21;
